ISO-10303-21;
HEADER;
FILE_DESCRIPTION (('STEP AP214'),
    '1' );
FILE_NAME ('Leaf Spring.step',
    '2026-10-06T10:23:46',
    ( '' ),
    ( '' ),
    'SwSTEP 2.0',
    'SolidWorks 2020',
    '' );
FILE_SCHEMA (( 'AUTOMOTIVE_DESIGN' ));
ENDSEC;

DATA;
#37=CARTESIAN_POINT ( 'NONE',  ( 33.31606138205700773, -26.06829118875199569, 75.80501292736998664 ) ) ;
#65=DIRECTION ( 'NONE',  ( 0.000000000000000000, 1.000000000000000000, -2.775557561562891351E-15 ) ) ;
#74=DIRECTION ( 'NONE',  ( 0.000000000000000000, -0.5735764363510444941, 0.8191520442889929088 ) ) ;
#86=ORIENTED_EDGE ( 'NONE', *, *, #3104, .F. ) ;
#107=LINE ( 'NONE', #13782, #2826 ) ;
#127=DIRECTION ( 'NONE',  ( 0.000000000000000000, 1.000000000000000000, -2.775557561562891351E-15 ) ) ;
#172=( GEOMETRIC_REPRESENTATION_CONTEXT ( 3 ) GLOBAL_UNCERTAINTY_ASSIGNED_CONTEXT ( ( #8249 ) ) GLOBAL_UNIT_ASSIGNED_CONTEXT ( ( #2358, #16143, #22073 ) ) REPRESENTATION_CONTEXT ( 'NONE', 'WORKASPACE' ) );
#175=FILL_AREA_STYLE ('',( #23869 ) ) ;
#191=EDGE_LOOP ( 'NONE', ( #11726, #12081, #22272, #24674 ) ) ;
#200=CARTESIAN_POINT ( 'NONE',  ( 37.42719827050449055, -22.02795882147844964, 75.81186121921504650 ) ) ;
#208=LINE ( 'NONE', #4092, #1342 ) ;
#211=ADVANCED_FACE ( 'NONE', ( #19460 ), #5431, .T. ) ;
#247=CARTESIAN_POINT ( 'NONE',  ( 39.93368021267864520, -5.986475166052370511, 82.77450256188085120 ) ) ;
#269=VECTOR ( 'NONE', #16270, 1000.000000000000000 ) ;
#283=ADVANCED_FACE ( 'NONE', ( #13171 ), #7751, .T. ) ;
#292=VECTOR ( 'NONE', #25323, 1000.000000000000000 ) ;
#312=VECTOR ( 'NONE', #16987, 1000.000000000000000 ) ;
#321=CARTESIAN_POINT ( 'NONE',  ( 36.37840728046802496, -20.80847383641847870, 75.91491741683218208 ) ) ;
#331=LINE ( 'NONE', #20056, #8211 ) ;
#336=EDGE_CURVE ( 'NONE', #3808, #21524, #7738, .T. ) ;
#353=VECTOR ( 'NONE', #14172, 1000.000000000000000 ) ;
#361=CARTESIAN_POINT ( 'NONE',  ( 39.82744760895728575, -21.57196225014778790, 75.82680905536302873 ) ) ;
#382=CARTESIAN_POINT ( 'NONE',  ( 33.31606138205700773, -16.48551471403133206, 77.11349248448009064 ) ) ;
#396=APPLICATION_CONTEXT ( 'automotive_design' ) ;
#450=CARTESIAN_POINT ( 'NONE',  ( 36.31606138205700063, -20.32227907754186802, 76.00185088427946312 ) ) ;
#461=DIRECTION ( 'NONE',  ( -0.000000000000000000, 0.1904761904761826663, -0.9816918156232541381 ) ) ;
#471=ORIENTED_EDGE ( 'NONE', *, *, #5498, .T. ) ;
#475=DIRECTION ( 'NONE',  ( 0.000000000000000000, 1.000000000000000000, -2.775557561562891351E-15 ) ) ;
#487=DIRECTION ( 'NONE',  ( -1.000000000000000000, 0.000000000000000000, 0.000000000000000000 ) ) ;
#490=CARTESIAN_POINT ( 'NONE',  ( 38.83707137437546919, -22.15663359646540087, 75.30013868356464002 ) ) ;
#500=DIRECTION ( 'NONE',  ( 1.000000000000000000, 0.000000000000000000, 0.000000000000000000 ) ) ;
#536=VERTEX_POINT ( 'NONE', #10946 ) ;
#563=ORIENTED_EDGE ( 'NONE', *, *, #20158, .T. ) ;
#582=EDGE_LOOP ( 'NONE', ( #9120, #20144, #14940, #6594 ) ) ;
#588=CIRCLE ( 'NONE', #8830, 10.00000000000000000 ) ;
#597=CARTESIAN_POINT ( 'NONE',  ( 36.57685537766501227, -21.21804332987624875, 75.35486877457063315 ) ) ;
#617=ORIENTED_EDGE ( 'NONE', *, *, #1775, .T. ) ;
#618=CARTESIAN_POINT ( 'NONE',  ( 40.31606138205700773, -20.48183877227857508, 75.44871329660013259 ) ) ;
#670=CYLINDRICAL_SURFACE ( 'NONE', #10166, 9.500000000000000000 ) ;
#678=CARTESIAN_POINT ( 'NONE',  ( 38.31606138205700063, -22.22127907754186893, 75.80501292736997243 ) ) ;
#697=VECTOR ( 'NONE', #20975, 999.9999999999998863 ) ;
#703=ORIENTED_EDGE ( 'NONE', *, *, #3804, .F. ) ;
#706=FACE_OUTER_BOUND ( 'NONE', #16935, .T. ) ;
#715=CARTESIAN_POINT ( 'NONE',  ( 37.09022467844553006, -21.80678508585893027, 75.31333329042418256 ) ) ;
#723=VERTEX_POINT ( 'NONE', #8092 ) ;
#740=CARTESIAN_POINT ( 'NONE',  ( 40.21566563214662438, -6.499520549983879292, 82.71640034338507519 ) ) ;
#742=EDGE_LOOP ( 'NONE', ( #8248, #22273, #16316, #86 ) ) ;
#743=CARTESIAN_POINT ( 'NONE',  ( 39.32240756636089429, -21.95458418863069028, 75.30830412695317477 ) ) ;
#756=CARTESIAN_POINT ( 'NONE',  ( 40.30296647725818104, -6.854917929055414305, 82.66861761357043292 ) ) ;
#766=CARTESIAN_POINT ( 'NONE',  ( 39.82744760895728575, -21.57196225014778790, 75.82680905536302873 ) ) ;
#787=DIRECTION ( 'NONE',  ( 0.000000000000000000, 1.861251128379125107E-14, 1.000000000000000000 ) ) ;
#812=EDGE_CURVE ( 'NONE', #17171, #21810, #20825, .T. ) ;
#838=CARTESIAN_POINT ( 'NONE',  ( 36.58819418470650220, -6.140949260442095436, 82.76158051492357970 ) ) ;
#865=CARTESIAN_POINT ( 'NONE',  ( 40.26527270485448184, -20.73887650502739177, 75.40739922272783247 ) ) ;
#891=EDGE_CURVE ( 'NONE', #14769, #4753, #6782, .T. ) ;
#906=ORIENTED_EDGE ( 'NONE', *, *, #891, .T. ) ;
#919=CARTESIAN_POINT ( 'NONE',  ( 38.18494427818247061, -22.22127907754186893, 75.81001292736998209 ) ) ;
#976=ADVANCED_FACE ( 'NONE', ( #13727 ), #1722, .T. ) ;
#1024=CARTESIAN_POINT ( 'NONE',  ( 39.32240756636089429, -21.96791893307624832, 75.80813956697402034 ) ) ;
#1049=FACE_OUTER_BOUND ( 'NONE', #24533, .T. ) ;
#1064=CARTESIAN_POINT ( 'NONE',  ( 36.31606138205700063, -20.44477830400171570, 75.97174273075597739 ) ) ;
#1078=FILL_AREA_STYLE_COLOUR ( '', #9416 ) ;
#1097=EDGE_LOOP ( 'NONE', ( #15045, #20610, #9343, #11397 ) ) ;
#1099=AXIS2_PLACEMENT_3D ( 'NONE', #3019, #12833, #12963 ) ;
#1106=ORIENTED_EDGE ( 'NONE', *, *, #17612, .T. ) ;
#1113=FACE_OUTER_BOUND ( 'NONE', #12163, .T. ) ;
#1174=CARTESIAN_POINT ( 'NONE',  ( 36.32862050049384806, -20.47881959453051692, 75.45202403124359591 ) ) ;
#1239=EDGE_CURVE ( 'NONE', #16406, #17655, #12232, .T. ) ;
#1249=AXIS2_PLACEMENT_3D ( 'NONE', #3363, #10974, #11240 ) ;
#1273=DIRECTION ( 'NONE',  ( 0.000000000000000000, 0.8191520442889929088, 0.5735764363510444941 ) ) ;
#1277=FACE_OUTER_BOUND ( 'NONE', #6390, .T. ) ;
#1283=CARTESIAN_POINT ( 'NONE',  ( 43.31606138205700063, -5.204193249396356968, 72.80501292736992980 ) ) ;
#1286=CARTESIAN_POINT ( 'NONE',  ( 38.83707137437546919, -22.15989686853476925, 75.80517981147842477 ) ) ;
#1294=CARTESIAN_POINT ( 'NONE',  ( 33.31606138205700773, -16.48551471403133206, 77.11349248448009064 ) ) ;
#1305=CARTESIAN_POINT ( 'NONE',  ( 43.31606138205700063, -4.357181138186123626, 83.30501292736992980 ) ) ;
#1308=PLANE ( 'NONE',  #18193 ) ;
#1312=DIRECTION ( 'NONE',  ( 0.000000000000000000, 1.000000000000000000, -2.999999999999999839E-15 ) ) ;
#1326=CARTESIAN_POINT ( 'NONE',  ( 37.67019652925851148, -5.306827745754475245, 83.30968309601763622 ) ) ;
#1340=CYLINDRICAL_SURFACE ( 'NONE', #15171, 9.500000000000000000 ) ;
#1342=VECTOR ( 'NONE', #18259, 1000.000000000000000 ) ;
#1347=ORIENTED_EDGE ( 'NONE', *, *, #10592, .F. ) ;
#1357=AXIS2_PLACEMENT_3D ( 'NONE', #18223, #4569, #15775 ) ;
#1391=CYLINDRICAL_SURFACE ( 'NONE', #18031, 10.00000000000000000 ) ;
#1399=CIRCLE ( 'NONE', #21957, 9.500000000000000000 ) ;
#1423=EDGE_LOOP ( 'NONE', ( #13555, #11688, #6031, #1794, #7597, #21299, #9719 ) ) ;
#1430=DIRECTION ( 'NONE',  ( 0.000000000000000000, -2.999999999999999839E-15, -1.000000000000000000 ) ) ;
#1438=CARTESIAN_POINT ( 'NONE',  ( 37.66883992158368955, -22.11817844025888036, 75.30541813598723877 ) ) ;
#1455=CARTESIAN_POINT ( 'NONE',  ( 36.31606138205700063, -7.205155154158177311, 83.11773453508298815 ) ) ;
#1500=EDGE_CURVE ( 'NONE', #14863, #19510, #21440, .T. ) ;
#1501=CARTESIAN_POINT ( 'NONE',  ( 39.91050633825327054, -5.952338289763780210, 82.77753289558458505 ) ) ;
#1546=DIRECTION ( 'NONE',  ( 0.000000000000000000, -2.999999999999999839E-15, -1.000000000000000000 ) ) ;
#1551=CARTESIAN_POINT ( 'NONE',  ( 36.99021717747880444, -21.72411701483781954, 75.31188971341042304 ) ) ;
#1583=VECTOR ( 'NONE', #20621, 1000.000000000000000 ) ;
#1625=CARTESIAN_POINT ( 'NONE',  ( 40.31606138205700773, -7.074889544382876316, 83.14300977595306108 ) ) ;
#1630=CARTESIAN_POINT ( 'NONE',  ( 43.31606138205700063, -10.93995761290683255, 80.99653337025984001 ) ) ;
#1676=EDGE_CURVE ( 'NONE', #14477, #21091, #11447, .T. ) ;
#1691=CARTESIAN_POINT ( 'NONE',  ( 36.72255525790973252, -5.988568098966074338, 83.27624199006054084 ) ) ;
#1693=VECTOR ( 'NONE', #3885, 999.9999999999998863 ) ;
#1722=CYLINDRICAL_SURFACE ( 'NONE', #2331, 3.000000000000002665 ) ;
#1725=ADVANCED_FACE ( 'NONE', ( #4177 ), #13962, .T. ) ;
#1737=AXIS2_PLACEMENT_3D ( 'NONE', #20070, #12488, #3306 ) ;
#1739=VERTEX_POINT ( 'NONE', #16385 ) ;
#1753=CARTESIAN_POINT ( 'NONE',  ( 38.83610899671118943, -5.268488250605326328, 83.30484769703562620 ) ) ;
#1764=ORIENTED_EDGE ( 'NONE', *, *, #2611, .T. ) ;
#1770=AXIS2_PLACEMENT_3D ( 'NONE', #4688, #22333, #14849 ) ;
#1775=EDGE_CURVE ( 'NONE', #8838, #3808, #2852, .T. ) ;
#1786=CARTESIAN_POINT ( 'NONE',  ( 36.36697178183959522, -6.685332804587225120, 83.20286675510105567 ) ) ;
#1790=CARTESIAN_POINT ( 'NONE',  ( 38.58006293444520196, -22.20877047264255921, 75.80998976194723582 ) ) ;
#1794=ORIENTED_EDGE ( 'NONE', *, *, #22157, .T. ) ;
#1798=ORIENTED_EDGE ( 'NONE', *, *, #18346, .T. ) ;
#1886=B_SPLINE_SURFACE_WITH_KNOTS ( 'NONE', 1, 3, ( 
 ( #15714, #17656, #1790, #15958, #7735, #23691, #4256, #14041, #15580, #23814, #9682, #13787, #23438, #21896, #12126, #23564 ),
 ( #19703, #2050, #17787, #19968, #2299, #10174, #16089, #12243, #12507, #361, #24310, #6815, #10304, #12376, #6679, #14660 ),
 ( #14542, #8755, #22401, #6437, #8245, #18415, #743, #22524, #6314, #16333, #4628, #4751, #20216, #8499, #4504, #14175 ),
 ( #10559, #4878, #24184, #490, #12756, #2552, #10434, #2929, #24442, #23939, #18537, #22020, #18295, #865, #618, #4381 ) ),
 .UNSPECIFIED., .F., .F., .F.,
 ( 2, 1, 1, 2 ),
 ( 4, 2, 2, 2, 2, 2, 2, 4 ),
 ( -0.01000000000000000021, 0.000000000000000000, 1.000000000000000000, 1.010099999999999998 ),
 ( 0.003140158914087874936, 0.003532297574693944991, 0.003924436235300010276, 0.004316574895906080331, 0.004708713556512150386, 0.005100852217118210033, 0.005492990877724280088, 0.006277268198936420199 ),
 .UNSPECIFIED. ) ;
#1950=CARTESIAN_POINT ( 'NONE',  ( 43.31606138205700063, -5.204193249396280585, 82.80501292736992980 ) ) ;
#1991=VECTOR ( 'NONE', #3346, 1000.000000000000000 ) ;
#2000=AXIS2_PLACEMENT_3D ( 'NONE', #9286, #12766, #22537 ) ;
#2003=CARTESIAN_POINT ( 'NONE',  ( 36.37840728046802496, -20.80772986314773831, 75.90997265879607880 ) ) ;
#2050=CARTESIAN_POINT ( 'NONE',  ( 38.44690133353662276, -22.22127907754186893, 75.80501292736997243 ) ) ;
#2072=VECTOR ( 'NONE', #5525, 1000.000000000000000 ) ;
#2080=DIRECTION ( 'NONE',  ( 1.000000000000000000, 0.000000000000000000, 0.000000000000000000 ) ) ;
#2108=DIRECTION ( 'NONE',  ( 1.000000000000000000, 0.000000000000000000, 0.000000000000000000 ) ) ;
#2122=EDGE_LOOP ( 'NONE', ( #4301, #13864, #16625, #3133 ) ) ;
#2123=FACE_OUTER_BOUND ( 'NONE', #15305, .T. ) ;
#2129=CARTESIAN_POINT ( 'NONE',  ( 36.80559154321147020, -21.57317817398384108, 75.83174599736526034 ) ) ;
#2145=ADVANCED_FACE ( 'NONE', ( #24993 ), #7380, .T. ) ;
#2147=EDGE_CURVE ( 'NONE', #21524, #17894, #4402, .T. ) ;
#2149=CARTESIAN_POINT ( 'NONE',  ( 36.98894827842408262, -21.72323602677954923, 75.31699084059582106 ) ) ;
#2156=VERTEX_POINT ( 'NONE', #9482 ) ;
#2189=DIRECTION ( 'NONE',  ( 0.000000000000000000, 1.000000000000000000, -2.775557561562891351E-15 ) ) ;
#2272=DIRECTION ( 'NONE',  ( 0.000000000000000000, -2.999999999999999839E-15, -1.000000000000000000 ) ) ;
#2276=CARTESIAN_POINT ( 'NONE',  ( 37.48451232389217580, -22.04143432302674555, 75.30659729247206258 ) ) ;
#2278=EDGE_LOOP ( 'NONE', ( #13540, #2635, #12420, #15880 ) ) ;
#2281=ORIENTED_EDGE ( 'NONE', *, *, #15480, .T. ) ;
#2299=CARTESIAN_POINT ( 'NONE',  ( 38.96215273200666473, -22.12375471166958008, 75.80539210339577494 ) ) ;
#2305=PRODUCT ( 'Leaf Spring', 'Leaf Spring', '', ( #24242 ) ) ;
#2313=ADVANCED_FACE ( 'NONE', ( #5860 ), #25412, .F. ) ;
#2331=AXIS2_PLACEMENT_3D ( 'NONE', #17338, #25419, #5366 ) ;
#2349=CARTESIAN_POINT ( 'NONE',  ( 33.31606138205700773, -26.06829118875200635, 72.80501292736998664 ) ) ;
#2358=( LENGTH_UNIT ( ) NAMED_UNIT ( * ) SI_UNIT ( .MILLI., .METRE. ) );
#2361=FACE_OUTER_BOUND ( 'NONE', #20310, .T. ) ;
#2374=EDGE_CURVE ( 'NONE', #14477, #15409, #8051, .T. ) ;
#2381=LINE ( 'NONE', #4202, #9181 ) ;
#2392=ADVANCED_FACE ( 'NONE', ( #10112 ), #20018, .T. ) ;
#2417=LINE ( 'NONE', #10295, #3390 ) ;
#2423=FACE_OUTER_BOUND ( 'NONE', #7251, .T. ) ;
#2425=AXIS2_PLACEMENT_3D ( 'NONE', #11642, #15614, #23466 ) ;
#2439=CARTESIAN_POINT ( 'NONE',  ( 38.57646292309977554, -5.204259650130242498, 82.80501292736988717 ) ) ;
#2464=ADVANCED_FACE ( 'NONE', ( #8174 ), #670, .F. ) ;
#2470=CIRCLE ( 'NONE', #5777, 3.000000000000002665 ) ;
#2482=CARTESIAN_POINT ( 'NONE',  ( 36.31606138205700063, -4.357181138186127178, 82.80501292736992980 ) ) ;
#2552=CARTESIAN_POINT ( 'NONE',  ( 39.20536636138601949, -22.01741677639897077, 75.30191219513037026 ) ) ;
#2596=CARTESIAN_POINT ( 'NONE',  ( 43.31606138205700063, -22.22127907754187959, 75.30501292736998664 ) ) ;
#2609=CARTESIAN_POINT ( 'NONE',  ( 33.31606138205700773, -22.22127907754180853, 85.30501292736998664 ) ) ;
#2611=EDGE_CURVE ( 'NONE', #23726, #17894, #3379, .T. ) ;
#2620=FACE_OUTER_BOUND ( 'NONE', #14305, .T. ) ;
#2626=ORIENTED_EDGE ( 'NONE', *, *, #22495, .F. ) ;
#2635=ORIENTED_EDGE ( 'NONE', *, *, #25431, .F. ) ;
#2647=DIRECTION ( 'NONE',  ( 0.000000000000000000, -0.8191520442889929088, -0.5735764363510444941 ) ) ;
#2655=CARTESIAN_POINT ( 'NONE',  ( 36.31606138205702905, -20.48366339139476011, 75.45349498244979713 ) ) ;
#2666=DIRECTION ( 'NONE',  ( 0.000000000000000000, -2.999999999999999839E-15, -1.000000000000000000 ) ) ;
#2735=DIRECTION ( 'NONE',  ( -0.000000000000000000, 1.000000000000000000, -3.225463739888140187E-15 ) ) ;
#2737=CARTESIAN_POINT ( 'NONE',  ( 37.42710149357921523, -5.397995270288631353, 82.79824951560235036 ) ) ;
#2754=VECTOR ( 'NONE', #18406, 1000.000000000000114 ) ;
#2764=DIRECTION ( 'NONE',  ( 0.000000000000000000, 2.999999999999999839E-15, 1.000000000000000000 ) ) ;
#2801=AXIS2_PLACEMENT_3D ( 'NONE', #4759, #500, #20478 ) ;
#2826=VECTOR ( 'NONE', #10298, 1000.000000000000000 ) ;
#2843=EDGE_LOOP ( 'NONE', ( #20394, #14541, #4813, #5088, #18954 ) ) ;
#2848=CARTESIAN_POINT ( 'NONE',  ( 37.31068429205632953, -21.96869763794396846, 75.81311457127152664 ) ) ;
#2852=LINE ( 'NONE', #18974, #23354 ) ;
#2864=CARTESIAN_POINT ( 'NONE',  ( 36.51585873400316018, -6.269293087353179139, 82.74377462301856667 ) ) ;
#2901=ORIENTED_EDGE ( 'NONE', *, *, #5341, .F. ) ;
#2916=CARTESIAN_POINT ( 'NONE',  ( 40.31606138205700773, -1.357181138186128067, 82.80501292736991559 ) ) ;
#2917=CARTESIAN_POINT ( 'NONE',  ( 40.30346352106939634, -6.945422957003676956, 83.16042775478545934 ) ) ;
#2922=CARTESIAN_POINT ( 'NONE',  ( 38.96303889229209716, -5.302259509207527088, 82.79964613853329070 ) ) ;
#2929=CARTESIAN_POINT ( 'NONE',  ( 39.53940869104339839, -21.80867927670156803, 75.30820817392812216 ) ) ;
#2946=VERTEX_POINT ( 'NONE', #6582 ) ;
#2953=CARTESIAN_POINT ( 'NONE',  ( 38.31606138205700063, -22.22127907754186893, 75.80501292736997243 ) ) ;
#2963=CARTESIAN_POINT ( 'NONE',  ( 40.31606138205700773, -20.32127907754186680, 75.99695190479390305 ) ) ;
#2964=CIRCLE ( 'NONE', #1737, 10.00000000000000178 ) ;
#2997=CARTESIAN_POINT ( 'NONE',  ( 36.31606138205700063, -7.108002773205779334, 82.61702262452435264 ) ) ;
#3006=EDGE_LOOP ( 'NONE', ( #703, #13380, #8247, #6877 ) ) ;
#3019=CARTESIAN_POINT ( 'NONE',  ( 43.31606138205700063, -5.204193249396356968, 72.80501292736992980 ) ) ;
#3026=CARTESIAN_POINT ( 'NONE',  ( 33.31606138205700773, -29.06829118875199924, 75.80501292737000085 ) ) ;
#3034=CARTESIAN_POINT ( 'NONE',  ( 37.01167919801150674, -5.663575426409370728, 82.79453121852071718 ) ) ;
#3055=CARTESIAN_POINT ( 'NONE',  ( 39.54057891361352972, -5.617364314676576598, 83.29713963190137349 ) ) ;
#3056=CARTESIAN_POINT ( 'NONE',  ( 36.31606138205700063, -20.32127907754186680, 75.99695190479390305 ) ) ;
#3059=CARTESIAN_POINT ( 'NONE',  ( 40.21566563214662438, -6.500168537627977194, 82.72135851617947822 ) ) ;
#3084=DIRECTION ( 'NONE',  ( 0.000000000000000000, -1.000000000000000000, 4.625929269271485322E-15 ) ) ;
#3093=CARTESIAN_POINT ( 'NONE',  ( 39.92124728212843365, -21.44350662387563489, 75.33352358636996371 ) ) ;
#3098=EDGE_LOOP ( 'NONE', ( #5356, #25164, #8587, #6818 ) ) ;
#3102=PLANE ( 'NONE',  #1249 ) ;
#3104=EDGE_CURVE ( 'NONE', #14953, #4563, #18947, .T. ) ;
#3114=CARTESIAN_POINT ( 'NONE',  ( 36.99021717747880444, -21.72436795495472950, 75.31693369342355027 ) ) ;
#3125=EDGE_CURVE ( 'NONE', #24795, #21810, #17458, .T. ) ;
#3133=ORIENTED_EDGE ( 'NONE', *, *, #21482, .T. ) ;
#3228=FACE_OUTER_BOUND ( 'NONE', #2278, .T. ) ;
#3232=VERTEX_POINT ( 'NONE', #21131 ) ;
#3236=CARTESIAN_POINT ( 'NONE',  ( 38.05466885408097255, -22.20914808198024559, 75.80498909504116511 ) ) ;
#3252=EDGE_CURVE ( 'NONE', #2156, #11682, #22922, .T. ) ;
#3257=ADVANCED_FACE ( 'NONE', ( #7608 ), #3723, .F. ) ;
#3258=CARTESIAN_POINT ( 'NONE',  ( 36.36697178183959522, -6.686045162182824519, 83.20786762765629874 ) ) ;
#3306=DIRECTION ( 'NONE',  ( 0.000000000000000000, -1.000000000000000000, 4.163336342344336238E-15 ) ) ;
#3320=CARTESIAN_POINT ( 'NONE',  ( 38.96303889229209716, -5.307263880975074066, 83.30967742110996710 ) ) ;
#3346=DIRECTION ( 'NONE',  ( 1.000000000000000000, 0.000000000000000000, 0.000000000000000000 ) ) ;
#3363=CARTESIAN_POINT ( 'NONE',  ( 33.31606138205700773, -11.22674583108233115, 81.40610939240433197 ) ) ;
#3372=CARTESIAN_POINT ( 'NONE',  ( 36.51558096900348005, -21.10182828056061055, 75.36712134771262583 ) ) ;
#3375=CARTESIAN_POINT ( 'NONE',  ( 33.31606138205700773, -11.22674583108233115, 81.40610939240433197 ) ) ;
#3379=LINE ( 'NONE', #14595, #15106 ) ;
#3390=VECTOR ( 'NONE', #7193, 1000.000000000000000 ) ;
#3416=VECTOR ( 'NONE', #8746, 1000.000000000000000 ) ;
#3437=ORIENTED_EDGE ( 'NONE', *, *, #7893, .T. ) ;
#3446=EDGE_CURVE ( 'NONE', #14751, #24251, #107, .T. ) ;
#3451=CARTESIAN_POINT ( 'NONE',  ( 39.54057891361352972, -5.617563030284176584, 83.30218584522116032 ) ) ;
#3456=LINE ( 'NONE', #24558, #11519 ) ;
#3476=CARTESIAN_POINT ( 'NONE',  ( 36.31606138205700063, -7.204193249396275256, 83.11277699141410835 ) ) ;
#3481=LINE ( 'NONE', #16399, #18524 ) ;
#3498=CARTESIAN_POINT ( 'NONE',  ( 38.31606138205700063, -22.22127907754186893, 75.29996292736998953 ) ) ;
#3513=CARTESIAN_POINT ( 'NONE',  ( 37.42710149357921523, -5.398092219773776179, 82.80324863345541075 ) ) ;
#3515=ORIENTED_EDGE ( 'NONE', *, *, #23388, .T. ) ;
#3546=ORIENTED_EDGE ( 'NONE', *, *, #13010, .F. ) ;
#3563=CARTESIAN_POINT ( 'NONE',  ( 39.32110845963273960, -5.470149936707826122, 83.30695469465730696 ) ) ;
#3595=ADVANCED_FACE ( 'NONE', ( #4624 ), #14046, .T. ) ;
#3613=ORIENTED_EDGE ( 'NONE', *, *, #22495, .T. ) ;
#3632=CARTESIAN_POINT ( 'NONE',  ( 37.09309150775561648, -5.616297516291425929, 83.29717550927296088 ) ) ;
#3645=LINE ( 'NONE', #19752, #9608 ) ;
#3683=VERTEX_POINT ( 'NONE', #15041 ) ;
#3696=CARTESIAN_POINT ( 'NONE',  ( 39.82611197195675601, -5.886287209492222949, 83.28324666752695293 ) ) ;
#3713=ADVANCED_FACE ( 'NONE', ( #8212 ), #15810, .F. ) ;
#3723=PLANE ( 'NONE',  #5296 ) ;
#3760=DIRECTION ( 'NONE',  ( 1.000000000000000000, 0.000000000000000000, 0.000000000000000000 ) ) ;
#3763=CARTESIAN_POINT ( 'NONE',  ( 38.18531088334250967, -5.204193249396277032, 83.30501292736992980 ) ) ;
#3779=CARTESIAN_POINT ( 'NONE',  ( 36.31606138205700063, -22.22127907754180853, 85.30501292736998664 ) ) ;
#3788=CIRCLE ( 'NONE', #10792, 3.000000000000000000 ) ;
#3804=EDGE_CURVE ( 'NONE', #12702, #24067, #331, .T. ) ;
#3808=VERTEX_POINT ( 'NONE', #11471 ) ;
#3853=CIRCLE ( 'NONE', #12913, 3.000000000000000000 ) ;
#3885=DIRECTION ( 'NONE',  ( 0.000000000000000000, -0.5735764363510463815, 0.8191520442889914655 ) ) ;
#3955=CARTESIAN_POINT ( 'NONE',  ( 38.83610899671118943, -5.268488250605326328, 83.30484769703562620 ) ) ;
#3993=ORIENTED_EDGE ( 'NONE', *, *, #17052, .T. ) ;
#4015=DIRECTION ( 'NONE',  ( -1.000000000000000000, 0.000000000000000000, 0.000000000000000000 ) ) ;
#4092=CARTESIAN_POINT ( 'NONE',  ( 33.31606138205700773, -16.77230293220685198, 77.52306850662458260 ) ) ;
#4093=AXIS2_PLACEMENT_3D ( 'NONE', #6409, #16059, #19934 ) ;
#4124=DIRECTION ( 'NONE',  ( 0.000000000000000000, 2.999999999999999839E-15, 1.000000000000000000 ) ) ;
#4142=CARTESIAN_POINT ( 'NONE',  ( 40.31606138205700773, -7.108955154158179468, 82.62193108360246185 ) ) ;
#4177=FACE_OUTER_BOUND ( 'NONE', #16014, .T. ) ;
#4202=CARTESIAN_POINT ( 'NONE',  ( 40.31606138205700773, -29.06829118875199924, 75.80501292737000085 ) ) ;
#4226=CARTESIAN_POINT ( 'NONE',  ( 37.31134410486515662, -21.95164459809526747, 75.30860040717502102 ) ) ;
#4256=CARTESIAN_POINT ( 'NONE',  ( 39.32240756636089429, -21.96805228052070902, 75.81313792137423491 ) ) ;
#4264=AXIS2_PLACEMENT_3D ( 'NONE', #10981, #20778, #24737 ) ;
#4283=DIRECTION ( 'NONE',  ( 0.000000000000000000, -2.999999999999999839E-15, -1.000000000000000000 ) ) ;
#4301=ORIENTED_EDGE ( 'NONE', *, *, #7674, .F. ) ;
#4306=LINE ( 'NONE', #20006, #17403 ) ;
#4328=ORIENTED_EDGE ( 'NONE', *, *, #3125, .T. ) ;
#4352=AXIS2_PLACEMENT_3D ( 'NONE', #23544, #17253, #5914 ) ;
#4357=ORIENTED_EDGE ( 'NONE', *, *, #9749, .F. ) ;
#4381=CARTESIAN_POINT ( 'NONE',  ( 40.31606138205700773, -20.22026907754187164, 75.50210598695683473 ) ) ;
#4394=CARTESIAN_POINT ( 'NONE',  ( 40.21075434067961396, -6.485969576596928299, 82.72322597119108423 ) ) ;
#4402=LINE ( 'NONE', #382, #15917 ) ;
#4436=DIRECTION ( 'NONE',  ( 1.000000000000000000, 0.000000000000000000, 0.000000000000000000 ) ) ;
#4443=DIRECTION ( 'NONE',  ( 0.000000000000000000, -0.5735764363510441610, 0.8191520442889931308 ) ) ;
#4469=ORIENTED_EDGE ( 'NONE', *, *, #1500, .T. ) ;
#4476=ORIENTED_EDGE ( 'NONE', *, *, #11957, .F. ) ;
#4504=CARTESIAN_POINT ( 'NONE',  ( 40.31606138205700773, -20.48271674625588190, 75.45368821557958938 ) ) ;
#4538=DIRECTION ( 'NONE',  ( 1.000000000000000000, 0.000000000000000000, 0.000000000000000000 ) ) ;
#4563=VERTEX_POINT ( 'NONE', #7651 ) ;
#4569=DIRECTION ( 'NONE',  ( -1.000000000000000000, 0.000000000000000000, 0.000000000000000000 ) ) ;
#4582=FACE_OUTER_BOUND ( 'NONE', #13387, .T. ) ;
#4612=VERTEX_POINT ( 'NONE', #19234 ) ;
#4624=FACE_OUTER_BOUND ( 'NONE', #3006, .T. ) ;
#4626=PLANE ( 'NONE',  #21760 ) ;
#4628=CARTESIAN_POINT ( 'NONE',  ( 39.90994555940143584, -21.43641088028507014, 75.33526458429165018 ) ) ;
#4652=CARTESIAN_POINT ( 'NONE',  ( 39.20536636138601949, -22.02770764502952616, 75.80686379705316824 ) ) ;
#4658=LINE ( 'NONE', #20626, #5332 ) ;
#4688=CARTESIAN_POINT ( 'NONE',  ( 40.31606138205700773, -16.48551471403133206, 77.11349248448009064 ) ) ;
#4698=CARTESIAN_POINT ( 'NONE',  ( 36.41626118072728246, -20.92798318178700612, 75.89274454529751779 ) ) ;
#4730=CARTESIAN_POINT ( 'NONE',  ( 37.16487936434712935, -5.549719057258167609, 82.79909873374894858 ) ) ;
#4746=CARTESIAN_POINT ( 'NONE',  ( 33.31606138205700773, -22.22127907754186893, 75.80501292736997243 ) ) ;
#4751=CARTESIAN_POINT ( 'NONE',  ( 40.05426416818898616, -21.21910829294392897, 75.35475896931059481 ) ) ;
#4753=VERTEX_POINT ( 'NONE', #10476 ) ;
#4759=CARTESIAN_POINT ( 'NONE',  ( 36.31606138205700063, -5.204193249396356968, 72.80501292736992980 ) ) ;
#4766=CARTESIAN_POINT ( 'NONE',  ( 36.31606138205700063, -20.22127907754186893, 75.50705395623725735 ) ) ;
#4772=CARTESIAN_POINT ( 'NONE',  ( 39.90994555940143584, -21.47565429014790794, 75.83375200144557482 ) ) ;
#4812=CARTESIAN_POINT ( 'NONE',  ( 37.31068429205633663, -21.96856463034018248, 75.80811620457531319 ) ) ;
#4813=ORIENTED_EDGE ( 'NONE', *, *, #23388, .F. ) ;
#4829=AXIS2_PLACEMENT_3D ( 'NONE', #11054, #6805, #24303 ) ;
#4848=CARTESIAN_POINT ( 'NONE',  ( 36.96379791088226341, -5.704114881462953868, 82.79260900670682588 ) ) ;
#4852=ORIENTED_EDGE ( 'NONE', *, *, #11683, .F. ) ;
#4865=VECTOR ( 'NONE', #22494, 999.9999999999998863 ) ;
#4873=CARTESIAN_POINT ( 'NONE',  ( 39.82611197195675601, -5.853481738078078145, 82.77929352097653748 ) ) ;
#4874=LINE ( 'NONE', #9008, #312 ) ;
#4878=CARTESIAN_POINT ( 'NONE',  ( 38.44690133353662276, -22.22127907754186893, 75.29996292736998953 ) ) ;
#4889=CARTESIAN_POINT ( 'NONE',  ( 40.31606138205700773, -16.48551471403133206, 77.11349248448009064 ) ) ;
#4908=ORIENTED_EDGE ( 'NONE', *, *, #20594, .T. ) ;
#4914=AXIS2_PLACEMENT_3D ( 'NONE', #22390, #24547, #20584 ) ;
#4936=DIRECTION ( 'NONE',  ( 0.000000000000000000, -1.000000000000000000, 2.999999999999999839E-15 ) ) ;
#4949=ORIENTED_EDGE ( 'NONE', *, *, #2374, .F. ) ;
#4954=B_SPLINE_CURVE_WITH_KNOTS ( 'NONE', 3,
 ( #21010, #13408, #9547, #19078, #14821, #3093, #19322, #9304, #10964, #18952 ),
 .UNSPECIFIED., .F., .F.,
 ( 4, 2, 2, 2, 4 ),
 ( 0.000000000000000000, 0.2500000000000000000, 0.5000000000000000000, 0.7500000000000000000, 1.000000000000000000 ),
 .UNSPECIFIED. ) ;
#4980=ADVANCED_FACE ( 'NONE', ( #3228 ), #16764, .F. ) ;
#4997=CARTESIAN_POINT ( 'NONE',  ( 40.05520938202761982, -6.207949209480774222, 83.25749895850351834 ) ) ;
#5005=ADVANCED_FACE ( 'NONE', ( #13168 ), #3102, .T. ) ;
#5011=ORIENTED_EDGE ( 'NONE', *, *, #21302, .T. ) ;
#5021=ADVANCED_FACE ( 'NONE', ( #11615 ), #24982, .T. ) ;
#5036=DIRECTION ( 'NONE',  ( 1.000000000000000000, 0.000000000000000000, 0.000000000000000000 ) ) ;
#5054=AXIS2_PLACEMENT_3D ( 'NONE', #6425, #12110, #475 ) ;
#5056=CARTESIAN_POINT ( 'NONE',  ( 38.31606138205700063, -22.22127907754186893, 75.30501292736998664 ) ) ;
#5077=CARTESIAN_POINT ( 'NONE',  ( 37.42719827050449766, -22.02785702039574289, 75.80686219251248303 ) ) ;
#5079=EDGE_CURVE ( 'NONE', #15185, #4753, #17541, .T. ) ;
#5088=ORIENTED_EDGE ( 'NONE', *, *, #336, .T. ) ;
#5100=ORIENTED_EDGE ( 'NONE', *, *, #17141, .T. ) ;
#5116=CARTESIAN_POINT ( 'NONE',  ( 36.36850376183099343, -6.605053338531620355, 82.70927162624322193 ) ) ;
#5121=CARTESIAN_POINT ( 'NONE',  ( 38.31606138205700063, -5.204193249396277032, 83.05501292736992980 ) ) ;
#5148=UNCERTAINTY_MEASURE_WITH_UNIT (LENGTH_MEASURE( 1.000000000000000082E-05 ), #8304, 'distance_accuracy_value', 'NONE');
#5169=CARTESIAN_POINT ( 'NONE',  ( 37.79523030992096011, -5.268760358274976241, 83.30484586594928942 ) ) ;
#5190=CARTESIAN_POINT ( 'NONE',  ( 38.18494427818247061, -22.22127907754186893, 75.29996292736998953 ) ) ;
#5205=CARTESIAN_POINT ( 'NONE',  ( 37.09309150775561648, -5.616495718819777494, 83.30222173984805067 ) ) ;
#5212=ORIENTED_EDGE ( 'NONE', *, *, #20832, .T. ) ;
#5219=EDGE_CURVE ( 'NONE', #16943, #723, #2470, .T. ) ;
#5225=DIRECTION ( 'NONE',  ( 0.000000000000000000, 1.000000000000000000, -2.999999999999999839E-15 ) ) ;
#5267=VERTEX_POINT ( 'NONE', #10066 ) ;
#5296=AXIS2_PLACEMENT_3D ( 'NONE', #25088, #23431, #25484 ) ;
#5313=CARTESIAN_POINT ( 'NONE',  ( 36.80559154321147020, -21.53870835236226711, 75.32790188997692837 ) ) ;
#5318=ADVANCED_FACE ( 'NONE', ( #15966 ), #9938, .T. ) ;
#5331=CARTESIAN_POINT ( 'NONE',  ( 36.80507328770344344, -5.887556683877273045, 83.28823336106593445 ) ) ;
#5332=VECTOR ( 'NONE', #4538, 1000.000000000000000 ) ;
#5341=EDGE_CURVE ( 'NONE', #5590, #4612, #16069, .T. ) ;
#5347=DIRECTION ( 'NONE',  ( 0.000000000000000000, 0.8191520442889929088, 0.5735764363510444941 ) ) ;
#5356=ORIENTED_EDGE ( 'NONE', *, *, #23410, .T. ) ;
#5366=DIRECTION ( 'NONE',  ( 1.000000000000000000, 0.000000000000000000, 0.000000000000000000 ) ) ;
#5387=CARTESIAN_POINT ( 'NONE',  ( 38.31606138205700063, -5.204193249396277032, 83.30501292736992980 ) ) ;
#5431=CYLINDRICAL_SURFACE ( 'NONE', #24550, 3.000000000000002665 ) ;
#5437=CARTESIAN_POINT ( 'NONE',  ( 37.79585267494195477, -22.15694282365413059, 75.30518664689680008 ) ) ;
#5452=CARTESIAN_POINT ( 'NONE',  ( 38.05217264712879199, -5.216727773490275943, 82.80503503306502466 ) ) ;
#5469=VECTOR ( 'NONE', #11545, 1000.000000000000000 ) ;
#5471=AXIS2_PLACEMENT_3D ( 'NONE', #8163, #6100, #12170 ) ;
#5498=EDGE_CURVE ( 'NONE', #14863, #6167, #24316, .T. ) ;
#5519=CARTESIAN_POINT ( 'NONE',  ( 38.31606138205700063, -5.204193249396280585, 82.80501292736992980 ) ) ;
#5525=DIRECTION ( 'NONE',  ( 0.000000000000000000, -2.999999999999999839E-15, -1.000000000000000000 ) ) ;
#5535=FACE_OUTER_BOUND ( 'NONE', #20099, .T. ) ;
#5544=CARTESIAN_POINT ( 'NONE',  ( 37.42710149357921523, -5.407787168292675695, 83.30316041875967414 ) ) ;
#5590=VERTEX_POINT ( 'NONE', #5880 ) ;
#5632=ADVANCED_FACE ( 'NONE', ( #2123 ), #23382, .F. ) ;
#5635=CARTESIAN_POINT ( 'NONE',  ( 39.32110845963273960, -5.457363569681777271, 82.80205412878008531 ) ) ;
#5640=VERTEX_POINT ( 'NONE', #6009 ) ;
#5662=CARTESIAN_POINT ( 'NONE',  ( 37.31005363372398165, -5.470694883964326571, 83.30188305377672009 ) ) ;
#5674=VECTOR ( 'NONE', #2647, 1000.000000000000000 ) ;
#5705=CARTESIAN_POINT ( 'NONE',  ( 36.72255525790973252, -5.951216915653229300, 82.77761203469431450 ) ) ;
#5721=LINE ( 'NONE', #13584, #23202 ) ;
#5728=CARTESIAN_POINT ( 'NONE',  ( 40.31606138205700773, -22.22127907754180853, 85.30501292736998664 ) ) ;
#5731=CARTESIAN_POINT ( 'NONE',  ( 36.31606138205700063, -16.48551471403133206, 77.11349248448009064 ) ) ;
#5735=CARTESIAN_POINT ( 'NONE',  ( 33.31606138205700773, -5.204193249396356968, 72.80501292736992980 ) ) ;
#5749=CARTESIAN_POINT ( 'NONE',  ( 33.31606138205700773, -5.204193249396356968, 72.80501292736992980 ) ) ;
#5768=CARTESIAN_POINT ( 'NONE',  ( 40.05520938202761982, -6.208431968299676917, 83.26252610654707098 ) ) ;
#5775=ORIENTED_EDGE ( 'NONE', *, *, #13038, .F. ) ;
#5777=AXIS2_PLACEMENT_3D ( 'NONE', #6323, #16227, #17925 ) ;
#5860=FACE_OUTER_BOUND ( 'NONE', #191, .T. ) ;
#5880=CARTESIAN_POINT ( 'NONE',  ( 36.31606138205700063, -16.77230293220685198, 77.52306850662458260 ) ) ;
#5914=DIRECTION ( 'NONE',  ( 1.000000000000000000, 0.000000000000000000, 0.000000000000000000 ) ) ;
#5963=FACE_OUTER_BOUND ( 'NONE', #23640, .T. ) ;
#5991=SURFACE_STYLE_FILL_AREA ( #175 ) ;
#5993=ORIENTED_EDGE ( 'NONE', *, *, #20604, .F. ) ;
#6004=CARTESIAN_POINT ( 'NONE',  ( 43.31606138205700063, -22.22127907754187959, 75.30501292736998664 ) ) ;
#6007=ORIENTED_EDGE ( 'NONE', *, *, #12104, .T. ) ;
#6009=CARTESIAN_POINT ( 'NONE',  ( 43.31606138205700063, -10.93995761290683255, 80.99653337025984001 ) ) ;
#6017=ORIENTED_EDGE ( 'NONE', *, *, #17300, .T. ) ;
#6031=ORIENTED_EDGE ( 'NONE', *, *, #20435, .T. ) ;
#6100=DIRECTION ( 'NONE',  ( 0.000000000000000000, -2.999999999999999839E-15, -1.000000000000000000 ) ) ;
#6112=PRESENTATION_STYLE_ASSIGNMENT (( #14098 ) ) ;
#6129=UNCERTAINTY_MEASURE_WITH_UNIT (LENGTH_MEASURE( 1.000000000000000082E-05 ), #12706, 'distance_accuracy_value', 'NONE');
#6146=CIRCLE ( 'NONE', #7394, 10.50000000000000000 ) ;
#6159=CARTESIAN_POINT ( 'NONE',  ( 36.51582732573286449, -21.10256731895815463, 75.36702044841622694 ) ) ;
#6160=ORIENTED_EDGE ( 'NONE', *, *, #22164, .F. ) ;
#6167=VERTEX_POINT ( 'NONE', #21301 ) ;
#6190=ORIENTED_EDGE ( 'NONE', *, *, #13277, .T. ) ;
#6196=DIRECTION ( 'NONE',  ( -1.000000000000000000, 0.000000000000000000, 0.000000000000000000 ) ) ;
#6199=CARTESIAN_POINT ( 'NONE',  ( 39.89406713111731051, -5.936539503995411415, 82.77827728996761891 ) ) ;
#6213=FACE_OUTER_BOUND ( 'NONE', #10599, .T. ) ;
#6252=CYLINDRICAL_SURFACE ( 'NONE', #10051, 10.50000000000000000 ) ;
#6264=EDGE_CURVE ( 'NONE', #18120, #536, #8545, .T. ) ;
#6314=CARTESIAN_POINT ( 'NONE',  ( 39.64097644196145609, -21.72530145503456822, 75.31687860557157421 ) ) ;
#6323=CARTESIAN_POINT ( 'NONE',  ( 36.31606138205700063, -26.06829118875199569, 75.80501292736998664 ) ) ;
#6324=CARTESIAN_POINT ( 'NONE',  ( 33.31606138205700773, -22.22127907754180853, 85.30501292736998664 ) ) ;
#6327=CARTESIAN_POINT ( 'NONE',  ( 39.52152274622449113, -5.583621694698644333, 82.79804034237957922 ) ) ;
#6328=DIRECTION ( 'NONE',  ( -1.000000000000000000, 0.000000000000000000, 0.000000000000000000 ) ) ;
#6341=CARTESIAN_POINT ( 'NONE',  ( 40.31606138205700773, -7.204193249396275256, 83.11277699141410835 ) ) ;
#6390=EDGE_LOOP ( 'NONE', ( #7960, #14174, #20408, #21400 ) ) ;
#6409=CARTESIAN_POINT ( 'NONE',  ( 33.31606138205700773, -5.204193249396277032, 83.30501292736992980 ) ) ;
#6421=EDGE_CURVE ( 'NONE', #17758, #2946, #18966, .T. ) ;
#6425=CARTESIAN_POINT ( 'NONE',  ( 33.31606138205700773, -22.22127907754180853, 85.30501292736998664 ) ) ;
#6433=DIRECTION ( 'NONE',  ( 0.000000000000000000, 1.000000000000000000, -2.921639538487253867E-15 ) ) ;
#6434=CARTESIAN_POINT ( 'NONE',  ( 40.31606138205700773, -26.06829118875199569, 75.80501292736998664 ) ) ;
#6437=CARTESIAN_POINT ( 'NONE',  ( 38.83707137437546919, -22.15666622595546187, 75.30518859485255234 ) ) ;
#6481=LINE ( 'NONE', #2349, #18689 ) ;
#6486=EDGE_LOOP ( 'NONE', ( #12335, #2281, #24714, #16092 ) ) ;
#6507=VECTOR ( 'NONE', #17711, 1000.000000000000000 ) ;
#6536=CIRCLE ( 'NONE', #2801, 10.00000000000000000 ) ;
#6553=CARTESIAN_POINT ( 'NONE',  ( 36.31606138205700063, -22.22127907754180853, 85.30501292736998664 ) ) ;
#6567=ORIENTED_EDGE ( 'NONE', *, *, #19313, .F. ) ;
#6582=CARTESIAN_POINT ( 'NONE',  ( 43.31606138205700063, -4.357181138186123626, 83.30501292736992980 ) ) ;
#6594=ORIENTED_EDGE ( 'NONE', *, *, #19634, .F. ) ;
#6615=PLANE ( 'NONE',  #1770 ) ;
#6621=CARTESIAN_POINT ( 'NONE',  ( 37.67019652925851148, -5.301844549589977973, 82.79965153790806198 ) ) ;
#6634=DIRECTION ( 'NONE',  ( 0.000000000000000000, 2.999999999999999839E-15, 1.000000000000000000 ) ) ;
#6651=CARTESIAN_POINT ( 'NONE',  ( 36.82041202018974957, -5.837982138606934157, 82.78530851280675051 ) ) ;
#6656=CARTESIAN_POINT ( 'NONE',  ( 33.31606138205700773, -22.22127907754187959, 75.30501292736998664 ) ) ;
#6673=AXIS2_PLACEMENT_3D ( 'NONE', #18288, #20079, #22264 ) ;
#6679=CARTESIAN_POINT ( 'NONE',  ( 40.31606138205700773, -20.56964486282017646, 75.94625445116911067 ) ) ;
#6732=DIRECTION ( 'NONE',  ( 0.000000000000000000, -2.999999999999999839E-15, -1.000000000000000000 ) ) ;
#6769=( NAMED_UNIT ( * ) SI_UNIT ( $, .STERADIAN. ) SOLID_ANGLE_UNIT ( ) );
#6782=B_SPLINE_CURVE_WITH_KNOTS ( 'NONE', 3,
 ( #7036, #12721, #9247, #18508, #14884, #12602, #6788, #4730, #20698, #3034, #4848, #6651, #10910, #838, #22372, #5116, #20438, #18761 ),
 .UNSPECIFIED., .F., .F.,
 ( 4, 2, 2, 2, 2, 2, 2, 2, 4 ),
 ( 0.000000000000000000, 0.1249999999999964473, 0.2499999999999928946, 0.3749999999999893419, 0.4374999999999907851, 0.4999999999999922284, 0.6249999999999952260, 0.7499999999999982236, 1.000000000000000000 ),
 .UNSPECIFIED. ) ;
#6788=CARTESIAN_POINT ( 'NONE',  ( 37.32688434004231937, -5.448512656755814199, 82.80225578647099383 ) ) ;
#6805=DIRECTION ( 'NONE',  ( -1.000000000000000000, 0.000000000000000000, 0.000000000000000000 ) ) ;
#6810=CARTESIAN_POINT ( 'NONE',  ( 40.30346352106939634, -6.861678099637780193, 82.66238161308596943 ) ) ;
#6815=CARTESIAN_POINT ( 'NONE',  ( 40.05426416818898616, -21.26921683217381798, 75.85227166721355729 ) ) ;
#6818=ORIENTED_EDGE ( 'NONE', *, *, #20976, .T. ) ;
#6824=DIRECTION ( 'NONE',  ( -1.000000000000000000, 0.000000000000000000, 0.000000000000000000 ) ) ;
#6841=EDGE_CURVE ( 'NONE', #24067, #14769, #7372, .T. ) ;
#6853=DIRECTION ( 'NONE',  ( 0.000000000000000000, 0.8191520442889929088, 0.5735764363510447161 ) ) ;
#6861=ADVANCED_FACE ( 'NONE', ( #1277 ), #11211, .T. ) ;
#6877=ORIENTED_EDGE ( 'NONE', *, *, #6841, .F. ) ;
#6916=EDGE_LOOP ( 'NONE', ( #10467, #12054, #20297, #8717 ) ) ;
#6935=CARTESIAN_POINT ( 'NONE',  ( 38.44711690269065940, -5.204193249396280585, 82.80001292736993435 ) ) ;
#6940=DIRECTION ( 'NONE',  ( 0.000000000000000000, -2.999999999999999839E-15, -1.000000000000000000 ) ) ;
#6953=ORIENTED_EDGE ( 'NONE', *, *, #1500, .F. ) ;
#6977=VERTEX_POINT ( 'NONE', #4889 ) ;
#7019=PRESENTATION_STYLE_ASSIGNMENT (( #14743 ) ) ;
#7036=CARTESIAN_POINT ( 'NONE',  ( 38.31606138205700063, -5.204193249396280585, 82.80501292736992980 ) ) ;
#7085=CARTESIAN_POINT ( 'NONE',  ( 40.31606138205700773, -4.357181138186123626, 83.30501292736992980 ) ) ;
#7099=ADVANCED_FACE ( 'NONE', ( #5535 ), #13517, .T. ) ;
#7102=DIRECTION ( 'NONE',  ( 0.000000000000000000, 0.8191520442889929088, 0.5735764363510447161 ) ) ;
#7117=CARTESIAN_POINT ( 'NONE',  ( 36.80559154321147020, -21.53836365414604614, 75.32286344890304974 ) ) ;
#7137=CARTESIAN_POINT ( 'NONE',  ( 33.31606138205700773, -16.48551471403133206, 77.11349248448009064 ) ) ;
#7142=AXIS2_PLACEMENT_3D ( 'NONE', #21664, #15983, #4283 ) ;
#7193=DIRECTION ( 'NONE',  ( 1.000000000000000000, 0.000000000000000000, 0.000000000000000000 ) ) ;
#7202=EDGE_CURVE ( 'NONE', #5640, #22871, #15324, .T. ) ;
#7207=EDGE_LOOP ( 'NONE', ( #6567, #15730, #8194, #15875, #23003 ) ) ;
#7246=CARTESIAN_POINT ( 'NONE',  ( 36.31606138205700063, -20.22026907754187164, 75.50210598695683473 ) ) ;
#7249=ADVANCED_FACE ( 'NONE', ( #20335 ), #20203, .T. ) ;
#7251=EDGE_LOOP ( 'NONE', ( #7681, #7442, #18934, #20003 ) ) ;
#7260=CARTESIAN_POINT ( 'NONE',  ( 38.05217264712879199, -5.217354499694973669, 83.30503613834979149 ) ) ;
#7273=DIRECTION ( 'NONE',  ( 1.000000000000000000, 0.000000000000000000, 0.000000000000000000 ) ) ;
#7320=CARTESIAN_POINT ( 'NONE',  ( 38.57734783014581836, -5.216950748870224253, 83.30503679799366523 ) ) ;
#7325=LINE ( 'NONE', #8887, #13170 ) ;
#7347=CARTESIAN_POINT ( 'NONE',  ( 43.31606138205700063, -22.22127907754180853, 85.30501292736998664 ) ) ;
#7372=B_SPLINE_CURVE_WITH_KNOTS ( 'NONE', 3,
 ( #4142, #10072, #756, #8644, #4394, #12139, #16474, #247, #6199, #10315, #23952, #14053, #6327, #14187, #12256, #20100, #2439, #18179 ),
 .UNSPECIFIED., .F., .F.,
 ( 4, 2, 2, 2, 2, 2, 2, 2, 4 ),
 ( 0.000000000000000000, 0.1250000000000000833, 0.2500000000000001665, 0.3750000000000002220, 0.4375000000000030531, 0.5000000000000058842, 0.6250000000000059952, 0.7500000000000061062, 1.000000000000000000 ),
 .UNSPECIFIED. ) ;
#7373=EDGE_CURVE ( 'NONE', #723, #14751, #11048, .T. ) ;
#7374=EDGE_CURVE ( 'NONE', #24769, #21641, #22739, .T. ) ;
#7375=CARTESIAN_POINT ( 'NONE',  ( 37.09113907096683960, -21.82847486639042955, 75.81287845682257398 ) ) ;
#7380=PLANE ( 'NONE',  #13868 ) ;
#7389=CIRCLE ( 'NONE', #9853, 3.000000000000002665 ) ;
#7393=CARTESIAN_POINT ( 'NONE',  ( 38.31606138205700063, -5.204193249396277032, 83.30501292736992980 ) ) ;
#7394=AXIS2_PLACEMENT_3D ( 'NONE', #7477, #5036, #9174 ) ;
#7399=VERTEX_POINT ( 'NONE', #20580 ) ;
#7442=ORIENTED_EDGE ( 'NONE', *, *, #17056, .F. ) ;
#7446=CARTESIAN_POINT ( 'NONE',  ( 38.83610899671118943, -5.265426583881079203, 82.80485556514678080 ) ) ;
#7477=CARTESIAN_POINT ( 'NONE',  ( 36.31606138205700063, -5.204193249396356968, 72.80501292736992980 ) ) ;
#7479=ORIENTED_EDGE ( 'NONE', *, *, #17781, .T. ) ;
#7522=ORIENTED_EDGE ( 'NONE', *, *, #21655, .F. ) ;
#7547=CARTESIAN_POINT ( 'NONE',  ( 33.31606138205700773, -5.204193249396277032, 83.30501292736992980 ) ) ;
#7577=ORIENTED_EDGE ( 'NONE', *, *, #10668, .T. ) ;
#7584=CARTESIAN_POINT ( 'NONE',  ( 40.31606138205700773, -7.073990261058225926, 83.13804008194063044 ) ) ;
#7590=ORIENTED_EDGE ( 'NONE', *, *, #3104, .T. ) ;
#7597=ORIENTED_EDGE ( 'NONE', *, *, #24233, .T. ) ;
#7608=FACE_OUTER_BOUND ( 'NONE', #24255, .T. ) ;
#7610=CARTESIAN_POINT ( 'NONE',  ( 36.72255525790973252, -5.988568098966074338, 83.27624199006054084 ) ) ;
#7646=CARTESIAN_POINT ( 'NONE',  ( 36.51585873400316018, -6.323645680884924403, 83.25095475337030848 ) ) ;
#7651=CARTESIAN_POINT ( 'NONE',  ( 43.31606138205700063, -26.06829118875199924, 75.30501292736998664 ) ) ;
#7674=EDGE_CURVE ( 'NONE', #1739, #24795, #23136, .T. ) ;
#7681=ORIENTED_EDGE ( 'NONE', *, *, #18303, .F. ) ;
#7699=CARTESIAN_POINT ( 'NONE',  ( 38.31606138205700063, -5.204193249396277032, 83.30501292736992980 ) ) ;
#7703=CARTESIAN_POINT ( 'NONE',  ( 40.11623881305710881, -6.323557511870723680, 83.25096693106735302 ) ) ;
#7735=CARTESIAN_POINT ( 'NONE',  ( 38.96215273200666473, -22.12380604028318842, 75.81039190382944071 ) ) ;
#7738=CIRCLE ( 'NONE', #15546, 10.00000000000000000 ) ;
#7751=CYLINDRICAL_SURFACE ( 'NONE', #15524, 3.000000000000002665 ) ;
#7769=LINE ( 'NONE', #10209, #14379 ) ;
#7773=CARTESIAN_POINT ( 'NONE',  ( 37.31005363372398165, -5.470694883964326571, 83.30188305377672009 ) ) ;
#7809=ORIENTED_EDGE ( 'NONE', *, *, #9920, .F. ) ;
#7816=ORIENTED_EDGE ( 'NONE', *, *, #23410, .F. ) ;
#7837=ADVANCED_FACE ( 'NONE', ( #10737 ), #21646, .F. ) ;
#7840=ADVANCED_FACE ( 'NONE', ( #1049 ), #1308, .F. ) ;
#7886=DIRECTION ( 'NONE',  ( 0.000000000000000000, -1.000000000000000000, 4.625929269271485322E-15 ) ) ;
#7893=EDGE_CURVE ( 'NONE', #11682, #17758, #20653, .T. ) ;
#7897=FACE_OUTER_BOUND ( 'NONE', #16176, .T. ) ;
#7899=PLANE ( 'NONE',  #16844 ) ;
#7955=CARTESIAN_POINT ( 'NONE',  ( 36.31606138205700063, -20.44571330440884793, 75.97665497822788438 ) ) ;
#7960=ORIENTED_EDGE ( 'NONE', *, *, #3252, .F. ) ;
#7999=LINE ( 'NONE', #13912, #19315 ) ;
#8043=CARTESIAN_POINT ( 'NONE',  ( 33.31606138205700773, -29.06829118875199924, 75.80501292737000085 ) ) ;
#8051=LINE ( 'NONE', #14347, #269 ) ;
#8053=( NAMED_UNIT ( * ) SI_UNIT ( $, .STERADIAN. ) SOLID_ANGLE_UNIT ( ) );
#8087=CARTESIAN_POINT ( 'NONE',  ( 40.31606138205700773, -1.357181138186128067, 82.80501292736991559 ) ) ;
#8092=CARTESIAN_POINT ( 'NONE',  ( 36.31606138205700063, -29.06829118875199924, 75.80501292737000085 ) ) ;
#8095=ORIENTED_EDGE ( 'NONE', *, *, #12104, .F. ) ;
#8101=VERTEX_POINT ( 'NONE', #4766 ) ;
#8163=CARTESIAN_POINT ( 'NONE',  ( 40.31606138205700773, -26.06829118875199924, 75.30501292736998664 ) ) ;
#8173=PLANE ( 'NONE',  #20724 ) ;
#8174=FACE_OUTER_BOUND ( 'NONE', #11170, .T. ) ;
#8194=ORIENTED_EDGE ( 'NONE', *, *, #6841, .T. ) ;
#8201=CARTESIAN_POINT ( 'NONE',  ( 36.72121174906109786, -21.47489429109494807, 75.83882253612472368 ) ) ;
#8211=VECTOR ( 'NONE', #461, 999.9999999999998863 ) ;
#8212=FACE_OUTER_BOUND ( 'NONE', #17272, .T. ) ;
#8245=CARTESIAN_POINT ( 'NONE',  ( 38.96215273200666473, -22.11862185030787842, 75.30541206002871490 ) ) ;
#8247=ORIENTED_EDGE ( 'NONE', *, *, #17847, .T. ) ;
#8248=ORIENTED_EDGE ( 'NONE', *, *, #22157, .F. ) ;
#8249=UNCERTAINTY_MEASURE_WITH_UNIT (LENGTH_MEASURE( 1.000000000000000082E-05 ), #2358, 'distance_accuracy_value', 'NONE');
#8265=AXIS2_PLACEMENT_3D ( 'NONE', #17796, #23822, #127 ) ;
#8304=( LENGTH_UNIT ( ) NAMED_UNIT ( * ) SI_UNIT ( .MILLI., .METRE. ) );
#8310=LINE ( 'NONE', #15780, #20549 ) ;
#8316=ORIENTED_EDGE ( 'NONE', *, *, #5079, .T. ) ;
#8335=ORIENTED_EDGE ( 'NONE', *, *, #3252, .T. ) ;
#8400=AXIS2_PLACEMENT_3D ( 'NONE', #7347, #21252, #11091 ) ;
#8472=CARTESIAN_POINT ( 'NONE',  ( 38.31606138205700063, -22.22127907754186893, 75.30501292736998664 ) ) ;
#8487=EDGE_CURVE ( 'NONE', #14769, #22871, #18154, .T. ) ;
#8499=CARTESIAN_POINT ( 'NONE',  ( 40.26527270485448184, -20.73962474046760818, 75.41239499478379571 ) ) ;
#8545=LINE ( 'NONE', #2596, #19514 ) ;
#8566=CARTESIAN_POINT ( 'NONE',  ( 38.18531088334250967, -5.204193249396280585, 82.80001292736993435 ) ) ;
#8579=ORIENTED_EDGE ( 'NONE', *, *, #22941, .F. ) ;
#8587=ORIENTED_EDGE ( 'NONE', *, *, #20594, .F. ) ;
#8591=DIRECTION ( 'NONE',  ( 0.000000000000000000, -1.000000000000000000, 2.999999999999999839E-15 ) ) ;
#8594=CARTESIAN_POINT ( 'NONE',  ( 36.31606138205700063, -1.357181138186128067, 82.80501292736991559 ) ) ;
#8600=ORIENTED_EDGE ( 'NONE', *, *, #16178, .T. ) ;
#8604=STYLED_ITEM ( 'NONE', ( #7019 ), #25265 ) ;
#8622=CARTESIAN_POINT ( 'NONE',  ( 40.11623881305710881, -6.269209199194929027, 82.74378620945387297 ) ) ;
#8626=EDGE_CURVE ( 'NONE', #15409, #11682, #24684, .T. ) ;
#8632=ORIENTED_EDGE ( 'NONE', *, *, #1775, .F. ) ;
#8640=AXIS2_PLACEMENT_3D ( 'NONE', #5735, #13099, #25418 ) ;
#8644=CARTESIAN_POINT ( 'NONE',  ( 40.25058685806286007, -6.608132892505640399, 82.70675736217422980 ) ) ;
#8654=ADVANCED_FACE ( 'NONE', ( #1113 ), #14534, .T. ) ;
#8664=CARTESIAN_POINT ( 'NONE',  ( 33.31606138205700773, -5.204193249396280585, 82.80501292736992980 ) ) ;
#8677=ORIENTED_EDGE ( 'NONE', *, *, #22941, .T. ) ;
#8696=DIRECTION ( 'NONE',  ( 1.000000000000000000, 0.000000000000000000, 0.000000000000000000 ) ) ;
#8698=CARTESIAN_POINT ( 'NONE',  ( 37.31005363372398165, -5.457877424396979649, 82.79703358579240557 ) ) ;
#8701=ORIENTED_EDGE ( 'NONE', *, *, #21723, .F. ) ;
#8717=ORIENTED_EDGE ( 'NONE', *, *, #7374, .T. ) ;
#8746=DIRECTION ( 'NONE',  ( 0.000000000000000000, 1.000000000000000000, -2.999999999999999839E-15 ) ) ;
#8755=CARTESIAN_POINT ( 'NONE',  ( 38.44690133353662276, -22.22127907754186893, 75.30501292736998664 ) ) ;
#8774=EDGE_LOOP ( 'NONE', ( #14646, #6017, #15771, #1764 ) ) ;
#8798=ORIENTED_EDGE ( 'NONE', *, *, #21655, .T. ) ;
#8809=EDGE_CURVE ( 'NONE', #24769, #24795, #16652, .T. ) ;
#8811=CARTESIAN_POINT ( 'NONE',  ( 36.31606138205700063, -20.32127907754186680, 75.99695190479390305 ) ) ;
#8827=CARTESIAN_POINT ( 'NONE',  ( 36.32862050049384806, -20.56677809167894466, 75.94939806155714734 ) ) ;
#8830=AXIS2_PLACEMENT_3D ( 'NONE', #3779, #13712, #11664 ) ;
#8838=VERTEX_POINT ( 'NONE', #15096 ) ;
#8860=EDGE_CURVE ( 'NONE', #6167, #16406, #14712, .T. ) ;
#8877=DIRECTION ( 'NONE',  ( 0.000000000000000000, -2.999999999999999839E-15, -1.000000000000000000 ) ) ;
#8882=CARTESIAN_POINT ( 'NONE',  ( 39.64148445914975127, -5.676854949425127472, 82.78922245135619562 ) ) ;
#8887=CARTESIAN_POINT ( 'NONE',  ( 43.31606138205700063, -5.204193249396277032, 83.30501292736992980 ) ) ;
#8908=CARTESIAN_POINT ( 'NONE',  ( 39.53940869104339839, -21.82950711158638768, 75.81284195793978142 ) ) ;
#8912=DIRECTION ( 'NONE',  ( -0.000000000000000000, 1.000000000000000000, -3.225463739888140187E-15 ) ) ;
#8928=CARTESIAN_POINT ( 'NONE',  ( 36.99021717747880444, -21.74921351108408984, 75.81633765512088985 ) ) ;
#8978=DIRECTION ( 'NONE',  ( 0.000000000000000000, 1.000000000000000000, -2.643388153869420409E-15 ) ) ;
#9008=CARTESIAN_POINT ( 'NONE',  ( 33.31606138205700773, -16.77230293220685198, 77.52306850662458260 ) ) ;
#9067=CARTESIAN_POINT ( 'NONE',  ( 36.72121174906109786, -21.47450125013314803, 75.83383770706140581 ) ) ;
#9084=AXIS2_PLACEMENT_3D ( 'NONE', #13418, #9691, #1430 ) ;
#9103=ORIENTED_EDGE ( 'NONE', *, *, #14752, .T. ) ;
#9120=ORIENTED_EDGE ( 'NONE', *, *, #10668, .F. ) ;
#9137=CARTESIAN_POINT ( 'NONE',  ( 40.21566563214662438, -6.564967302039574903, 83.21717579561996558 ) ) ;
#9157=CARTESIAN_POINT ( 'NONE',  ( 43.31606138205700063, -11.22674583108233115, 81.40610939240433197 ) ) ;
#9165=FACE_OUTER_BOUND ( 'NONE', #10096, .T. ) ;
#9174=DIRECTION ( 'NONE',  ( 0.000000000000000000, 1.000000000000000000, -2.643388153869420409E-15 ) ) ;
#9181=VECTOR ( 'NONE', #6634, 1000.000000000000000 ) ;
#9183=ORIENTED_EDGE ( 'NONE', *, *, #18222, .F. ) ;
#9191=DIRECTION ( 'NONE',  ( 0.000000000000000000, 2.999999999999999839E-15, 1.000000000000000000 ) ) ;
#9197=DIRECTION ( 'NONE',  ( 1.000000000000000000, 0.000000000000000000, 0.000000000000000000 ) ) ;
#9212=CARTESIAN_POINT ( 'NONE',  ( 37.79523030992096011, -5.268760358274976241, 83.30484586594928942 ) ) ;
#9217=ORIENTED_EDGE ( 'NONE', *, *, #21219, .F. ) ;
#9247=CARTESIAN_POINT ( 'NONE',  ( 38.05805554829457549, -5.215892093002847396, 82.80503322521296639 ) ) ;
#9255=STYLED_ITEM ( 'NONE', ( #6112 ), #20268 ) ;
#9270=CARTESIAN_POINT ( 'NONE',  ( 40.30346352106939634, -6.946260405577324271, 83.16540821620245083 ) ) ;
#9286=CARTESIAN_POINT ( 'NONE',  ( 0.000000000000000000, 0.000000000000000000, 0.000000000000000000 ) ) ;
#9304=CARTESIAN_POINT ( 'NONE',  ( 40.26596246014180736, -20.73830680248926228, 75.41253730274715394 ) ) ;
#9309=FACE_OUTER_BOUND ( 'NONE', #20732, .T. ) ;
#9321=CARTESIAN_POINT ( 'NONE',  ( 38.05466885408097255, -22.20850960852963851, 75.30498784070806551 ) ) ;
#9335=CARTESIAN_POINT ( 'NONE',  ( 37.79523030992096011, -5.265685734042680366, 82.80485382125503691 ) ) ;
#9343=ORIENTED_EDGE ( 'NONE', *, *, #17612, .F. ) ;
#9347=LINE ( 'NONE', #16939, #22156 ) ;
#9355=ADVANCED_FACE ( 'NONE', ( #9165 ), #14944, .F. ) ;
#9385=LINE ( 'NONE', #11325, #292 ) ;
#9387=CARTESIAN_POINT ( 'NONE',  ( 38.31606138205700063, -5.204193249396277032, 83.30501292736992980 ) ) ;
#9390=CARTESIAN_POINT ( 'NONE',  ( 39.64148445914975127, -5.700975119520175660, 83.29872180780533597 ) ) ;
#9391=LINE ( 'NONE', #17237, #9824 ) ;
#9396=CARTESIAN_POINT ( 'NONE',  ( 43.31606138205700063, -29.06829118875199924, 75.80501292737000085 ) ) ;
#9416=COLOUR_RGB ( '', 0.72549020, 0.75294118, 0.79215686) ;
#9442=CARTESIAN_POINT ( 'NONE',  ( 37.42719827050449055, -22.01757409303136015, 75.30191050528723906 ) ) ;
#9455=AXIS2_PLACEMENT_3D ( 'NONE', #12091, #12346, #2272 ) ;
#9459=CARTESIAN_POINT ( 'NONE',  ( 37.31005363372398165, -5.458004329937278243, 82.80203209537640419 ) ) ;
#9482=CARTESIAN_POINT ( 'NONE',  ( 36.31606138205700063, -1.357181138186128067, 82.80501292736991559 ) ) ;
#9520=CARTESIAN_POINT ( 'NONE',  ( 38.31606138205700063, -5.204193249396277032, 83.31006292736994112 ) ) ;
#9521=CARTESIAN_POINT ( 'NONE',  ( 33.31606138205700773, -5.204193249396356968, 72.80501292736992980 ) ) ;
#9522=B_SPLINE_SURFACE_WITH_KNOTS ( 'NONE', 1, 3, ( 
 ( #12572, #8566, #16401, #24250, #6621, #2737, #8698, #16529, #22461, #12691, #22589, #20531, #2864, #20663, #18596, #2997 ),
 ( #18731, #16791, #5452, #9335, #25129, #3513, #9459, #19358, #21046, #11267, #5705, #9710, #22844, #15237, #11518, #13567 ),
 ( #7393, #3763, #7260, #9212, #13067, #18986, #7773, #3632, #15363, #24881, #1691, #20918, #23091, #17061, #15111, #22968 ),
 ( #17437, #21291, #19116, #25264, #1326, #9586, #15487, #5205, #17561, #5331, #13322, #21174, #7646, #3258, #11388, #1455 ) ),
 .UNSPECIFIED., .F., .F., .F.,
 ( 2, 1, 1, 2 ),
 ( 4, 2, 2, 2, 2, 2, 2, 4 ),
 ( -0.01000000000000000021, 0.000000000000000000, 1.000000000000000000, 1.010099999999999998 ),
 ( 0.003138930853187265040, 0.003530919451234335038, 0.003922908049281400265, 0.004314896647328465493, 0.004706885245375529853, 0.005098873843422600284, 0.005490862441469669848, 0.006274839637563800303 ),
 .UNSPECIFIED. ) ;
#9547=CARTESIAN_POINT ( 'NONE',  ( 38.83857451401112826, -22.17007608312400890, 75.30462120507141321 ) ) ;
#9560=B_SPLINE_CURVE_WITH_KNOTS ( 'NONE', 3,
 ( #14266, #2655, #20323, #6159, #597, #19810, #20064, #2149, #715, #22118, #4226, #24042, #2276, #10030, #14145, #8472 ),
 .UNSPECIFIED., .F., .F.,
 ( 4, 2, 2, 2, 2, 2, 2, 4 ),
 ( 0.000000000000000000, 0.2499999999999884537, 0.3749999999999854006, 0.4999999999999823475, 0.6249999999999793499, 0.6874999999999815703, 0.7499999999999837907, 1.000000000000000000 ),
 .UNSPECIFIED. ) ;
#9563=DIRECTION ( 'NONE',  ( -1.000000000000000000, 0.000000000000000000, 0.000000000000000000 ) ) ;
#9586=CARTESIAN_POINT ( 'NONE',  ( 37.42710149357921523, -5.407885087272725322, 83.30820952779124866 ) ) ;
#9608=VECTOR ( 'NONE', #23103, 1000.000000000000000 ) ;
#9613=DIRECTION ( 'NONE',  ( 0.000000000000000000, -2.999999999999999839E-15, -1.000000000000000000 ) ) ;
#9643=CIRCLE ( 'NONE', #8400, 10.00000000000000000 ) ;
#9651=CARTESIAN_POINT ( 'NONE',  ( 40.31606138205700773, -7.205155154158177311, 83.11773453508298815 ) ) ;
#9656=LINE ( 'NONE', #11841, #2072 ) ;
#9682=CARTESIAN_POINT ( 'NONE',  ( 39.90994555940143584, -21.47604672424653671, 75.83873687561711563 ) ) ;
#9691=DIRECTION ( 'NONE',  ( 1.000000000000000000, 0.000000000000000000, 0.000000000000000000 ) ) ;
#9710=CARTESIAN_POINT ( 'NONE',  ( 36.57819145821473228, -6.158092363301129524, 82.75995410217588244 ) ) ;
#9719=ORIENTED_EDGE ( 'NONE', *, *, #8809, .F. ) ;
#9749=EDGE_CURVE ( 'NONE', #21524, #3232, #2417, .T. ) ;
#9768=DIRECTION ( 'NONE',  ( 0.000000000000000000, 1.000000000000000000, -2.775557561562891351E-15 ) ) ;
#9771=DIRECTION ( 'NONE',  ( 0.000000000000000000, -2.999999999999999839E-15, -1.000000000000000000 ) ) ;
#9824=VECTOR ( 'NONE', #25063, 1000.000000000000000 ) ;
#9835=EDGE_LOOP ( 'NONE', ( #18573, #10473, #19979, #14237 ) ) ;
#9846=ORIENTED_EDGE ( 'NONE', *, *, #7373, .T. ) ;
#9853=AXIS2_PLACEMENT_3D ( 'NONE', #6434, #4124, #16214 ) ;
#9867=ORIENTED_EDGE ( 'NONE', *, *, #3446, .T. ) ;
#9907=AXIS2_PLACEMENT_3D ( 'NONE', #10855, #10728, #13036 ) ;
#9912=EDGE_CURVE ( 'NONE', #16943, #24769, #24686, .T. ) ;
#9920=EDGE_CURVE ( 'NONE', #12702, #11458, #11444, .T. ) ;
#9938=CYLINDRICAL_SURFACE ( 'NONE', #8265, 10.00000000000000000 ) ;
#10011=CARTESIAN_POINT ( 'NONE',  ( 37.09113907096683960, -21.82868160544892788, 75.81787431707023472 ) ) ;
#10030=CARTESIAN_POINT ( 'NONE',  ( 37.79221860075193717, -22.16980752718048464, 75.30461792607815141 ) ) ;
#10051=AXIS2_PLACEMENT_3D ( 'NONE', #20410, #21967, #12449 ) ;
#10066=CARTESIAN_POINT ( 'NONE',  ( 43.31606138205700063, -16.48551471403133206, 77.11349248448009064 ) ) ;
#10072=CARTESIAN_POINT ( 'NONE',  ( 40.31606138205700063, -6.980777400833622970, 82.64680122081715297 ) ) ;
#10073=DIRECTION ( 'NONE',  ( 0.000000000000000000, -1.000000000000000000, 2.643388153869420804E-15 ) ) ;
#10082=VECTOR ( 'NONE', #11253, 1000.000000000000000 ) ;
#10096=EDGE_LOOP ( 'NONE', ( #16643, #15844, #15923, #13219 ) ) ;
#10108=DIRECTION ( 'NONE',  ( 1.000000000000000000, 0.000000000000000000, 0.000000000000000000 ) ) ;
#10112=FACE_OUTER_BOUND ( 'NONE', #9835, .T. ) ;
#10152=DIRECTION ( 'NONE',  ( 0.000000000000000000, 1.000000000000000000, -2.999999999999999839E-15 ) ) ;
#10166=AXIS2_PLACEMENT_3D ( 'NONE', #2609, #4436, #12302 ) ;
#10174=CARTESIAN_POINT ( 'NONE',  ( 39.20536636138601949, -22.02770764502952616, 75.80686379705316824 ) ) ;
#10207=AXIS2_PLACEMENT_3D ( 'NONE', #14341, #21817, #10108 ) ;
#10209=CARTESIAN_POINT ( 'NONE',  ( 33.31606138205700773, -29.06829118875199924, 75.80501292737000085 ) ) ;
#10295=CARTESIAN_POINT ( 'NONE',  ( 33.31606138205700773, -16.48551471403133206, 77.11349248448009064 ) ) ;
#10298=DIRECTION ( 'NONE',  ( 1.000000000000000000, 0.000000000000000000, 0.000000000000000000 ) ) ;
#10299=CARTESIAN_POINT ( 'NONE',  ( 33.31606138205700773, -11.22674583108233115, 81.40610939240433197 ) ) ;
#10304=CARTESIAN_POINT ( 'NONE',  ( 40.11656585159207822, -21.15771639874553500, 75.86402839307550039 ) ) ;
#10315=CARTESIAN_POINT ( 'NONE',  ( 39.80936209861184238, -5.840161863587774782, 82.78488652399678926 ) ) ;
#10434=CARTESIAN_POINT ( 'NONE',  ( 39.32240756636089429, -21.95444950771180004, 75.30325578900897199 ) ) ;
#10440=CIRCLE ( 'NONE', #12090, 10.49999999999999822 ) ;
#10467=ORIENTED_EDGE ( 'NONE', *, *, #17300, .F. ) ;
#10473=ORIENTED_EDGE ( 'NONE', *, *, #15691, .T. ) ;
#10476=CARTESIAN_POINT ( 'NONE',  ( 36.31606138205700063, -7.108955154158179468, 82.62193108360246185 ) ) ;
#10538=ORIENTED_EDGE ( 'NONE', *, *, #8860, .F. ) ;
#10555=CARTESIAN_POINT ( 'NONE',  ( 40.31606138205700773, -6.984061928592629975, 82.64107068069698414 ) ) ;
#10559=CARTESIAN_POINT ( 'NONE',  ( 38.31606138205700063, -22.22127907754186893, 75.29996292736998953 ) ) ;
#10577=VECTOR ( 'NONE', #13945, 1000.000000000000000 ) ;
#10592=EDGE_CURVE ( 'NONE', #4563, #18120, #13593, .T. ) ;
#10599=EDGE_LOOP ( 'NONE', ( #13786, #18127, #9217, #23110 ) ) ;
#10668=EDGE_CURVE ( 'NONE', #21783, #2156, #3853, .T. ) ;
#10681=CARTESIAN_POINT ( 'NONE',  ( 33.31606138205700773, -29.06829118875199924, 75.80501292737000085 ) ) ;
#10682=DIRECTION ( 'NONE',  ( 0.000000000000000000, -1.861251128379125107E-14, -1.000000000000000000 ) ) ;
#10689=EDGE_LOOP ( 'NONE', ( #21572, #11284, #11784, #4328 ) ) ;
#10715=CARTESIAN_POINT ( 'NONE',  ( 38.44690133353662276, -22.22127907754186893, 75.80501292736997243 ) ) ;
#10728=DIRECTION ( 'NONE',  ( -1.000000000000000000, 0.000000000000000000, 0.000000000000000000 ) ) ;
#10737=FACE_OUTER_BOUND ( 'NONE', #2122, .T. ) ;
#10744=ADVANCED_FACE ( 'NONE', ( #17969 ), #8173, .T. ) ;
#10792=AXIS2_PLACEMENT_3D ( 'NONE', #7085, #16879, #3084 ) ;
#10796=CARTESIAN_POINT ( 'NONE',  ( 36.31606138205700063, -29.06829118875199924, 75.80501292737000085 ) ) ;
#10838=CARTESIAN_POINT ( 'NONE',  ( 38.58006293444520196, -22.20876388569947935, 75.80498974974848636 ) ) ;
#10855=CARTESIAN_POINT ( 'NONE',  ( 36.31606138205700063, -5.204193249396356968, 72.80501292736992980 ) ) ;
#10879=CARTESIAN_POINT ( 'NONE',  ( 36.51558096900348005, -21.15780082040966903, 75.86401592669550098 ) ) ;
#10889=ORIENTED_EDGE ( 'NONE', *, *, #18763, .F. ) ;
#10895=MECHANICAL_DESIGN_GEOMETRIC_PRESENTATION_REPRESENTATION('',(#9255),#172);
#10898=VECTOR ( 'NONE', #9191, 1000.000000000000000 ) ;
#10905=VECTOR ( 'NONE', #9197, 1000.000000000000000 ) ;
#10908=LINE ( 'NONE', #10299, #18687 ) ;
#10910=CARTESIAN_POINT ( 'NONE',  ( 36.73573221557511204, -5.934306775458773053, 82.77886294573366399 ) ) ;
#10914=ORIENTED_EDGE ( 'NONE', *, *, #19001, .F. ) ;
#10932=LINE ( 'NONE', #4746, #17602 ) ;
#10935=CARTESIAN_POINT ( 'NONE',  ( 40.11623881305710881, -6.269741973556977044, 82.74875808203118766 ) ) ;
#10946=CARTESIAN_POINT ( 'NONE',  ( 43.31606138205700063, -22.22127907754186893, 75.80501292736997243 ) ) ;
#10964=CARTESIAN_POINT ( 'NONE',  ( 40.31606138205701484, -20.48435987709931183, 75.45335281290067542 ) ) ;
#10974=DIRECTION ( 'NONE',  ( -1.000000000000000000, 0.000000000000000000, 0.000000000000000000 ) ) ;
#10981=CARTESIAN_POINT ( 'NONE',  ( 40.31606138205700773, -5.204193249396356968, 72.80501292736992980 ) ) ;
#10984=CARTESIAN_POINT ( 'NONE',  ( 36.37840728046802496, -20.73258112307092915, 75.41050264957048910 ) ) ;
#11001=CARTESIAN_POINT ( 'NONE',  ( 36.99021717747880444, -21.74921351108408984, 75.81633765512088985 ) ) ;
#11028=ORIENTED_EDGE ( 'NONE', *, *, #8487, .F. ) ;
#11031=CARTESIAN_POINT ( 'NONE',  ( 40.31606138205700773, -22.22127907754180853, 85.30501292736998664 ) ) ;
#11048=LINE ( 'NONE', #10796, #19858 ) ;
#11053=CARTESIAN_POINT ( 'NONE',  ( 40.25357836725066818, -6.691594714027675472, 83.19992197100876297 ) ) ;
#11054=CARTESIAN_POINT ( 'NONE',  ( 40.31606138205700773, -5.204193249396356968, 72.80501292736992980 ) ) ;
#11091=DIRECTION ( 'NONE',  ( 0.000000000000000000, 1.000000000000000000, -2.775557561562891351E-15 ) ) ;
#11100=PLANE ( 'NONE',  #20120 ) ;
#11116=CARTESIAN_POINT ( 'NONE',  ( 36.37840728046802496, -20.73333253607436788, 75.41549685518693025 ) ) ;
#11118=CARTESIAN_POINT ( 'NONE',  ( 33.31606138205700773, -22.22127907754186893, 75.80501292736997243 ) ) ;
#11141=SHAPE_REPRESENTATION ( 'Leaf Spring', ( #2000 ), #17482 ) ;
#11163=ADVANCED_FACE ( 'NONE', ( #12233 ), #14411, .T. ) ;
#11170=EDGE_LOOP ( 'NONE', ( #12803, #2901, #4852, #22813, #17121 ) ) ;
#11211=PLANE ( 'NONE',  #15429 ) ;
#11231=VERTEX_POINT ( 'NONE', #14280 ) ;
#11240=DIRECTION ( 'NONE',  ( 0.000000000000000000, -1.000000000000000000, 2.999999999999999839E-15 ) ) ;
#11250=CARTESIAN_POINT ( 'NONE',  ( 38.18494427818247061, -22.22127907754186893, 75.80501292736997243 ) ) ;
#11253=DIRECTION ( 'NONE',  ( 1.000000000000000000, 0.000000000000000000, 0.000000000000000000 ) ) ;
#11267=CARTESIAN_POINT ( 'NONE',  ( 36.80507328770344344, -5.854702703878681191, 82.78423285844689872 ) ) ;
#11284=ORIENTED_EDGE ( 'NONE', *, *, #20832, .F. ) ;
#11304=ORIENTED_EDGE ( 'NONE', *, *, #12266, .F. ) ;
#11325=CARTESIAN_POINT ( 'NONE',  ( 33.31606138205700773, -22.22127907754186893, 75.80501292736997243 ) ) ;
#11372=CARTESIAN_POINT ( 'NONE',  ( 36.51558096900348005, -21.15780082040966903, 75.86401592669550098 ) ) ;
#11388=CARTESIAN_POINT ( 'NONE',  ( 36.31606138205700063, -6.943143338275722165, 83.16857229470855373 ) ) ;
#11397=ORIENTED_EDGE ( 'NONE', *, *, #6421, .F. ) ;
#11406=AXIS2_PLACEMENT_3D ( 'NONE', #1283, #22419, #12898 ) ;
#11441=CARTESIAN_POINT ( 'NONE',  ( 39.32110845963273960, -5.470022085696077063, 83.30190618885059450 ) ) ;
#11444=B_SPLINE_CURVE_WITH_KNOTS ( 'NONE', 3,
 ( #14786, #24302, #2917, #11053, #9137, #22644, #4997, #22892, #20974, #20718, #3055, #11441, #25321, #21609, #3955, #19284, #25057, #7699 ),
 .UNSPECIFIED., .F., .F.,
 ( 4, 2, 2, 2, 2, 2, 2, 2, 4 ),
 ( 0.000000000000000000, 0.1249999999999999445, 0.2499999999999998890, 0.3749999999999998335, 0.4999999999999991673, 0.6249999999999997780, 0.7500000000000003331, 0.8749999999999994449, 1.000000000000000000 ),
 .UNSPECIFIED. ) ;
#11447=CIRCLE ( 'NONE', #14716, 3.000000000000000000 ) ;
#11450=CARTESIAN_POINT ( 'NONE',  ( 38.44711690269065940, -5.204193249396280585, 82.80501292736992980 ) ) ;
#11458=VERTEX_POINT ( 'NONE', #9387 ) ;
#11471=CARTESIAN_POINT ( 'NONE',  ( 33.31606138205700773, -22.22127907754187959, 75.30501292736998664 ) ) ;
#11515=VECTOR ( 'NONE', #8877, 1000.000000000000000 ) ;
#11518=CARTESIAN_POINT ( 'NONE',  ( 36.31606138205700063, -6.859540048202029894, 82.67032472249573516 ) ) ;
#11519=VECTOR ( 'NONE', #6940, 1000.000000000000000 ) ;
#11541=DIRECTION ( 'NONE',  ( 1.000000000000000000, 0.000000000000000000, 0.000000000000000000 ) ) ;
#11545=DIRECTION ( 'NONE',  ( 1.000000000000000000, 0.000000000000000000, 0.000000000000000000 ) ) ;
#11562=ORIENTED_EDGE ( 'NONE', *, *, #25318, .T. ) ;
#11571=CARTESIAN_POINT ( 'NONE',  ( 38.31606138205700063, -22.22127907754186893, 75.55501292736998664 ) ) ;
#11578=CARTESIAN_POINT ( 'NONE',  ( 39.54057891361352972, -5.617364314676576598, 83.29713963190137349 ) ) ;
#11615=FACE_OUTER_BOUND ( 'NONE', #12788, .T. ) ;
#11642=CARTESIAN_POINT ( 'NONE',  ( 43.31606138205700063, -22.22127907754187959, 75.30501292736998664 ) ) ;
#11659=CARTESIAN_POINT ( 'NONE',  ( 40.31606138205700773, -1.357181138186124736, 83.30501292736991559 ) ) ;
#11660=FACE_OUTER_BOUND ( 'NONE', #20809, .T. ) ;
#11664=DIRECTION ( 'NONE',  ( 0.000000000000000000, 1.000000000000000000, -2.775557561562891351E-15 ) ) ;
#11667=CARTESIAN_POINT ( 'NONE',  ( 33.31606138205700773, -16.77230293220685198, 77.52306850662458260 ) ) ;
#11682=VERTEX_POINT ( 'NONE', #8087 ) ;
#11683=EDGE_CURVE ( 'NONE', #21641, #5590, #208, .T. ) ;
#11688=ORIENTED_EDGE ( 'NONE', *, *, #5219, .T. ) ;
#11720=VECTOR ( 'NONE', #74, 1000.000000000000000 ) ;
#11726=ORIENTED_EDGE ( 'NONE', *, *, #14752, .F. ) ;
#11784=ORIENTED_EDGE ( 'NONE', *, *, #7674, .T. ) ;
#11814=ORIENTED_EDGE ( 'NONE', *, *, #21150, .T. ) ;
#11824=CARTESIAN_POINT ( 'NONE',  ( 38.31606138205700063, -22.22127907754186893, 75.81001292736998209 ) ) ;
#11841=CARTESIAN_POINT ( 'NONE',  ( 33.31606138205700773, -4.357181138186130731, 81.40610939240430355 ) ) ;
#11867=FACE_OUTER_BOUND ( 'NONE', #10689, .T. ) ;
#11917=DIRECTION ( 'NONE',  ( 0.000000000000000000, -1.000000000000000000, 4.625929269271485322E-15 ) ) ;
#11928=PLANE ( 'NONE',  #20516 ) ;
#11957=EDGE_CURVE ( 'NONE', #3232, #5590, #13226, .T. ) ;
#11976=EDGE_LOOP ( 'NONE', ( #21178, #5775, #8095, #18343, #6190 ) ) ;
#11988=CARTESIAN_POINT ( 'NONE',  ( 33.31606138205700773, -5.204193249396280585, 82.80501292736992980 ) ) ;
#11995=LINE ( 'NONE', #19833, #353 ) ;
#12025=CARTESIAN_POINT ( 'NONE',  ( 43.31606138205700063, -10.93995761290683255, 80.99653337025984001 ) ) ;
#12034=ORIENTED_EDGE ( 'NONE', *, *, #13277, .F. ) ;
#12054=ORIENTED_EDGE ( 'NONE', *, *, #336, .F. ) ;
#12081=ORIENTED_EDGE ( 'NONE', *, *, #812, .T. ) ;
#12090=AXIS2_PLACEMENT_3D ( 'NONE', #17802, #6328, #10073 ) ;
#12091=CARTESIAN_POINT ( 'NONE',  ( 40.31606138205700773, -5.204193249396356968, 72.80501292736992980 ) ) ;
#12104=EDGE_CURVE ( 'NONE', #3683, #11458, #19140, .T. ) ;
#12110=DIRECTION ( 'NONE',  ( 1.000000000000000000, 0.000000000000000000, 0.000000000000000000 ) ) ;
#12126=CARTESIAN_POINT ( 'NONE',  ( 40.31606138205700773, -20.57051414398581812, 75.95118011352499821 ) ) ;
#12139=CARTESIAN_POINT ( 'NONE',  ( 40.10709070826256806, -6.251773263459675434, 82.75068920652414306 ) ) ;
#12163=EDGE_LOOP ( 'NONE', ( #21626, #19910, #2626, #14495 ) ) ;
#12170=DIRECTION ( 'NONE',  ( 1.000000000000000000, 0.000000000000000000, 0.000000000000000000 ) ) ;
#12179=DIRECTION ( 'NONE',  ( 0.000000000000000000, -3.289120579329467819E-15, -1.000000000000000000 ) ) ;
#12184=DIRECTION ( 'NONE',  ( 0.000000000000000000, -2.999999999999999839E-15, -1.000000000000000000 ) ) ;
#12215=FACE_OUTER_BOUND ( 'NONE', #6486, .T. ) ;
#12232=CIRCLE ( 'NONE', #1099, 10.49999999999999822 ) ;
#12233=FACE_OUTER_BOUND ( 'NONE', #24245, .T. ) ;
#12236=AXIS2_PLACEMENT_3D ( 'NONE', #5728, #11541, #9613 ) ;
#12243=CARTESIAN_POINT ( 'NONE',  ( 39.53940869104339839, -21.82950711158638768, 75.81284195793978142 ) ) ;
#12256=CARTESIAN_POINT ( 'NONE',  ( 39.18866295275135769, -5.390573154769174202, 82.80338437050654932 ) ) ;
#12266=EDGE_CURVE ( 'NONE', #17894, #19306, #21942, .T. ) ;
#12297=CARTESIAN_POINT ( 'NONE',  ( 36.31606138205700063, -4.357181138186123626, 83.30501292736992980 ) ) ;
#12302=DIRECTION ( 'NONE',  ( 0.000000000000000000, 1.000000000000000000, -2.921639538487253867E-15 ) ) ;
#12335=ORIENTED_EDGE ( 'NONE', *, *, #15930, .F. ) ;
#12345=VECTOR ( 'NONE', #14883, 1000.000000000000000 ) ;
#12346=DIRECTION ( 'NONE',  ( 1.000000000000000000, 0.000000000000000000, 0.000000000000000000 ) ) ;
#12353=ADVANCED_FACE ( 'NONE', ( #16395 ), #6615, .T. ) ;
#12375=EDGE_LOOP ( 'NONE', ( #8632, #5100, #24254, #1798 ) ) ;
#12376=CARTESIAN_POINT ( 'NONE',  ( 40.26527270485448184, -20.81370745732132832, 75.90702589141309886 ) ) ;
#12420=ORIENTED_EDGE ( 'NONE', *, *, #5079, .F. ) ;
#12441=CARTESIAN_POINT ( 'NONE',  ( 33.31606138205700773, -5.204193249396277032, 83.30501292736992980 ) ) ;
#12449=DIRECTION ( 'NONE',  ( 0.000000000000000000, 1.000000000000000000, -2.643388153869420409E-15 ) ) ;
#12457=FILL_AREA_STYLE ('',( #1078 ) ) ;
#12488=DIRECTION ( 'NONE',  ( 1.000000000000000000, 0.000000000000000000, 0.000000000000000000 ) ) ;
#12502=CARTESIAN_POINT ( 'NONE',  ( 40.31606138205700773, -7.108002773205779334, 82.61702262452435264 ) ) ;
#12507=CARTESIAN_POINT ( 'NONE',  ( 39.64097644196145609, -21.75010033615993876, 75.81628532166148204 ) ) ;
#12553=DIRECTION ( 'NONE',  ( 0.000000000000000000, 0.8191520442889929088, 0.5735764363510444941 ) ) ;
#12572=CARTESIAN_POINT ( 'NONE',  ( 38.31606138205700063, -5.204193249396280585, 82.80001292736993435 ) ) ;
#12592=ORIENTED_EDGE ( 'NONE', *, *, #5498, .F. ) ;
#12602=CARTESIAN_POINT ( 'NONE',  ( 37.44193150466009001, -5.391171257106773140, 82.80337612851013773 ) ) ;
#12603=ADVANCED_FACE ( 'NONE', ( #7897 ), #17944, .T. ) ;
#12615=DIRECTION ( 'NONE',  ( 0.000000000000000000, -1.000000000000000000, 4.382459307730880209E-15 ) ) ;
#12691=CARTESIAN_POINT ( 'NONE',  ( 36.80507328770344344, -5.854377449151428436, 82.77924324848135029 ) ) ;
#12702=VERTEX_POINT ( 'NONE', #6341 ) ;
#12706=( LENGTH_UNIT ( ) NAMED_UNIT ( * ) SI_UNIT ( .MILLI., .METRE. ) );
#12720=CARTESIAN_POINT ( 'NONE',  ( 43.31606138205700063, -5.204193249396280585, 82.80501292736992980 ) ) ;
#12721=CARTESIAN_POINT ( 'NONE',  ( 38.18583742984269946, -5.204226263507460537, 82.80501292736992980 ) ) ;
#12756=CARTESIAN_POINT ( 'NONE',  ( 38.96215273200666473, -22.11857000840811693, 75.30036226159070623 ) ) ;
#12766=DIRECTION ( 'NONE',  ( 0.000000000000000000, 0.000000000000000000, 1.000000000000000000 ) ) ;
#12788=EDGE_LOOP ( 'NONE', ( #25295, #7590, #23846, #24353 ) ) ;
#12799=CARTESIAN_POINT ( 'NONE',  ( 37.31068429205632953, -21.96856463034017892, 75.80811620457531319 ) ) ;
#12803=ORIENTED_EDGE ( 'NONE', *, *, #21482, .F. ) ;
#12816=CARTESIAN_POINT ( 'NONE',  ( 36.37840728046802496, -20.80772986314774187, 75.90997265879607880 ) ) ;
#12833=DIRECTION ( 'NONE',  ( -1.000000000000000000, 0.000000000000000000, 0.000000000000000000 ) ) ;
#12868=CARTESIAN_POINT ( 'NONE',  ( 40.31606138205700773, -6.984952308121978426, 82.64599116981820259 ) ) ;
#12898=DIRECTION ( 'NONE',  ( 0.000000000000000000, -1.000000000000000000, 2.999999999999999839E-15 ) ) ;
#12913=AXIS2_PLACEMENT_3D ( 'NONE', #2482, #12179, #16015 ) ;
#12915=ORIENTED_EDGE ( 'NONE', *, *, #8860, .T. ) ;
#12943=CARTESIAN_POINT ( 'NONE',  ( 37.79585267494195477, -22.16015963634850650, 75.80517796092046012 ) ) ;
#12957=SURFACE_SIDE_STYLE ('',( #16418 ) ) ;
#12963=DIRECTION ( 'NONE',  ( 0.000000000000000000, -1.000000000000000000, 2.643388153869420804E-15 ) ) ;
#12969=B_SPLINE_CURVE_WITH_KNOTS ( 'NONE', 3,
 ( #16886, #24966, #13024, #5169, #19317, #5544, #5662, #17393, #25226, #15193, #7610, #19440, #23049, #1786, #21133, #3476 ),
 .UNSPECIFIED., .F., .F.,
 ( 4, 2, 2, 2, 2, 2, 2, 4 ),
 ( 0.000000000000000000, 0.1250000000000009992, 0.2500000000000004441, 0.3749999999999998890, 0.4999999999999991118, 0.6250000000000002220, 0.7500000000000011102, 1.000000000000000000 ),
 .UNSPECIFIED. ) ;
#12983=LINE ( 'NONE', #5121, #24756 ) ;
#13005=ORIENTED_EDGE ( 'NONE', *, *, #13503, .T. ) ;
#13010=EDGE_CURVE ( 'NONE', #18120, #5267, #9643, .T. ) ;
#13022=CARTESIAN_POINT ( 'NONE',  ( 43.31606138205700063, -26.06829118875199214, 77.52306850662461102 ) ) ;
#13024=CARTESIAN_POINT ( 'NONE',  ( 38.05217264712879199, -5.217354499694973669, 83.30503613834979149 ) ) ;
#13036=DIRECTION ( 'NONE',  ( 0.000000000000000000, -1.000000000000000000, 2.999999999999999839E-15 ) ) ;
#13038=EDGE_CURVE ( 'NONE', #11458, #15185, #12969, .T. ) ;
#13048=CARTESIAN_POINT ( 'NONE',  ( 36.31606138205700063, -20.22127907754186893, 75.50705395623725735 ) ) ;
#13067=CARTESIAN_POINT ( 'NONE',  ( 37.67019652925851148, -5.306778407178573964, 83.30463327861060918 ) ) ;
#13099=DIRECTION ( 'NONE',  ( -1.000000000000000000, 0.000000000000000000, 0.000000000000000000 ) ) ;
#13124=CARTESIAN_POINT ( 'NONE',  ( 39.20459794252392527, -5.397949909403978452, 82.80325005500586144 ) ) ;
#13168=FACE_OUTER_BOUND ( 'NONE', #3098, .T. ) ;
#13170=VECTOR ( 'NONE', #20729, 1000.000000000000000 ) ;
#13171=FACE_OUTER_BOUND ( 'NONE', #582, .T. ) ;
#13178=CARTESIAN_POINT ( 'NONE',  ( 36.57656417722905928, -21.21691551846920731, 75.35497464634362075 ) ) ;
#13214=EDGE_CURVE ( 'NONE', #21810, #14863, #1399, .T. ) ;
#13219=ORIENTED_EDGE ( 'NONE', *, *, #21219, .T. ) ;
#13226=LINE ( 'NONE', #5731, #20696 ) ;
#13253=CARTESIAN_POINT ( 'NONE',  ( 40.21566563214662438, -6.565621769560124221, 83.22218355014231861 ) ) ;
#13277=EDGE_CURVE ( 'NONE', #23726, #7399, #10908, .T. ) ;
#13305=CARTESIAN_POINT ( 'NONE',  ( 37.42719827050449055, -22.02785702039573934, 75.80686219251248303 ) ) ;
#13322=CARTESIAN_POINT ( 'NONE',  ( 36.72255525790973252, -5.988945345917574770, 83.28127815260972966 ) ) ;
#13380=ORIENTED_EDGE ( 'NONE', *, *, #9920, .T. ) ;
#13384=CARTESIAN_POINT ( 'NONE',  ( 39.20459794252392527, -5.407735589517674413, 83.30821102113711163 ) ) ;
#13387=EDGE_LOOP ( 'NONE', ( #9183, #12915, #16461, #8579, #7809 ) ) ;
#13408=CARTESIAN_POINT ( 'NONE',  ( 38.58254500368953188, -22.22120764818083671, 75.30501292737000085 ) ) ;
#13418=CARTESIAN_POINT ( 'NONE',  ( 43.31606138205700063, -16.77230293220685198, 77.52306850662458260 ) ) ;
#13461=AXIS2_PLACEMENT_3D ( 'NONE', #23721, #2080, #17950 ) ;
#13499=CARTESIAN_POINT ( 'NONE',  ( 38.96303889229209716, -5.302308566866229533, 82.80464595504712122 ) ) ;
#13503=EDGE_CURVE ( 'NONE', #15622, #7399, #17741, .T. ) ;
#13517=PLANE ( 'NONE',  #4352 ) ;
#13531=ORIENTED_EDGE ( 'NONE', *, *, #20976, .F. ) ;
#13540=ORIENTED_EDGE ( 'NONE', *, *, #13503, .F. ) ;
#13555=ORIENTED_EDGE ( 'NONE', *, *, #9912, .F. ) ;
#13567=CARTESIAN_POINT ( 'NONE',  ( 36.31606138205700063, -7.108955154158179468, 82.62193108360246185 ) ) ;
#13568=VECTOR ( 'NONE', #4443, 1000.000000000000000 ) ;
#13584=CARTESIAN_POINT ( 'NONE',  ( 43.31606138205700063, -16.77230293220685198, 77.52306850662458260 ) ) ;
#13593=LINE ( 'NONE', #19511, #15361 ) ;
#13628=CARTESIAN_POINT ( 'NONE',  ( 40.30346352106939634, -6.945422957003676956, 83.16042775478545934 ) ) ;
#13654=ADVANCED_FACE ( 'NONE', ( #4582 ), #6252, .T. ) ;
#13712=DIRECTION ( 'NONE',  ( -1.000000000000000000, 0.000000000000000000, 0.000000000000000000 ) ) ;
#13727=FACE_OUTER_BOUND ( 'NONE', #1097, .T. ) ;
#13739=ORIENTED_EDGE ( 'NONE', *, *, #6264, .F. ) ;
#13748=CARTESIAN_POINT ( 'NONE',  ( 36.57656417722905928, -21.26763587820238044, 75.85745157953545004 ) ) ;
#13782=CARTESIAN_POINT ( 'NONE',  ( 33.31606138205700773, -29.06829118875199924, 75.30501292737000085 ) ) ;
#13786=ORIENTED_EDGE ( 'NONE', *, *, #21302, .F. ) ;
#13787=CARTESIAN_POINT ( 'NONE',  ( 40.05426416818898616, -21.26971791756611907, 75.85724679419259076 ) ) ;
#13864=ORIENTED_EDGE ( 'NONE', *, *, #24306, .F. ) ;
#13868=AXIS2_PLACEMENT_3D ( 'NONE', #15224, #4015, #24085 ) ;
#13893=CARTESIAN_POINT ( 'NONE',  ( 36.31606138205700063, -1.357181138186124736, 83.30501292736991559 ) ) ;
#13912=CARTESIAN_POINT ( 'NONE',  ( 33.31606138205700773, -5.204193249396280585, 82.80501292736992980 ) ) ;
#13945=DIRECTION ( 'NONE',  ( -0.000000000000000000, 1.000000000000000000, -3.225463739888140187E-15 ) ) ;
#13953=VECTOR ( 'NONE', #8912, 1000.000000000000000 ) ;
#13962=PLANE ( 'NONE',  #10207 ) ;
#13978=DIRECTION ( 'NONE',  ( 0.000000000000000000, -0.8191520442889929088, -0.5735764363510444941 ) ) ;
#14041=CARTESIAN_POINT ( 'NONE',  ( 39.53940869104339839, -21.82971330735793813, 75.81783783739737714 ) ) ;
#14046=B_SPLINE_SURFACE_WITH_KNOTS ( 'NONE', 1, 3, ( 
 ( #12502, #10555, #6810, #18530, #740, #8622, #16459, #14790, #4873, #8882, #20589, #24689, #24305, #2922, #16720, #24554, #6935, #14912 ),
 ( #22649, #12868, #20723, #22774, #3059, #10935, #18783, #1501, #15427, #15295, #23146, #5635, #13124, #13499, #7446, #17501, #11450, #5519 ),
 ( #23276, #7584, #13628, #25192, #23022, #17116, #21349, #19288, #3696, #19412, #11578, #19165, #24932, #17362, #1753, #7320, #25325, #5387 ),
 ( #9651, #1625, #9270, #20980, #13253, #7703, #5768, #15549, #21229, #9390, #3451, #3563, #13384, #3320, #21480, #23397, #21105, #9520 ) ),
 .UNSPECIFIED., .F., .F., .F.,
 ( 2, 1, 1, 2 ),
 ( 4, 2, 2, 2, 2, 2, 2, 2, 4 ),
 ( -0.01000000000000000021, 0.000000000000000000, 1.000000000000000000, 1.010099999999999998 ),
 ( 0.000000000000000000, 0.0003923663566484079674, 0.0007847327132968159348, 0.001177099069945223902, 0.001569465426593629918, 0.001961831783242040054, 0.002354198139890449973, 0.002746564496538855121, 0.003138930853187265040 ),
 .UNSPECIFIED. ) ;
#14053=CARTESIAN_POINT ( 'NONE',  ( 39.62251006394166097, -5.661281603007885188, 82.79494754200436546 ) ) ;
#14084=ORIENTED_EDGE ( 'NONE', *, *, #18763, .T. ) ;
#14098=SURFACE_STYLE_USAGE ( .BOTH. , #20020 ) ;
#14103=AXIS2_PLACEMENT_3D ( 'NONE', #18152, #17770, #23680 ) ;
#14145=CARTESIAN_POINT ( 'NONE',  ( 38.04888786834955994, -22.22120570019677288, 75.30501292736998664 ) ) ;
#14172=DIRECTION ( 'NONE',  ( 1.000000000000000000, 0.000000000000000000, 0.000000000000000000 ) ) ;
#14174=ORIENTED_EDGE ( 'NONE', *, *, #19634, .T. ) ;
#14175=CARTESIAN_POINT ( 'NONE',  ( 40.31606138205700773, -20.22127907754186893, 75.50705395623725735 ) ) ;
#14181=PRODUCT_DEFINITION_CONTEXT ( 'detailed design', #396, 'design' ) ;
#14187=CARTESIAN_POINT ( 'NONE',  ( 39.30543087153672843, -5.448589505030816404, 82.80225421346835901 ) ) ;
#14205=PLANE ( 'NONE',  #2425 ) ;
#14209=LINE ( 'NONE', #1950, #10577 ) ;
#14237=ORIENTED_EDGE ( 'NONE', *, *, #25318, .F. ) ;
#14266=CARTESIAN_POINT ( 'NONE',  ( 36.31606138205700063, -20.22127907754186893, 75.50705395623725735 ) ) ;
#14280=CARTESIAN_POINT ( 'NONE',  ( 40.31606138205700773, -10.93995761290683255, 80.99653337025984001 ) ) ;
#14305=EDGE_LOOP ( 'NONE', ( #18791, #15770, #8316, #19535 ) ) ;
#14341=CARTESIAN_POINT ( 'NONE',  ( 33.31606138205700773, -29.06829118875199924, 75.30501292737000085 ) ) ;
#14347=CARTESIAN_POINT ( 'NONE',  ( 33.31606138205700773, -1.357181138186124736, 83.30501292736991559 ) ) ;
#14349=SHAPE_REPRESENTATION_RELATIONSHIP ( 'NONE' , 'NONE' ,  #11141, #20268 ) ;
#14351=MECHANICAL_DESIGN_GEOMETRIC_PRESENTATION_REPRESENTATION('',(#8604),#23386);
#14379=VECTOR ( 'NONE', #19993, 1000.000000000000000 ) ;
#14411=PLANE ( 'NONE',  #6673 ) ;
#14466=DIRECTION ( 'NONE',  ( 0.000000000000000000, 2.999999999999999839E-15, 1.000000000000000000 ) ) ;
#14477=VERTEX_POINT ( 'NONE', #13893 ) ;
#14495=ORIENTED_EDGE ( 'NONE', *, *, #7373, .F. ) ;
#14529=DIRECTION ( 'NONE',  ( 1.000000000000000000, 0.000000000000000000, 0.000000000000000000 ) ) ;
#14534=CYLINDRICAL_SURFACE ( 'NONE', #4914, 3.000000000000002665 ) ;
#14541=ORIENTED_EDGE ( 'NONE', *, *, #24306, .T. ) ;
#14542=CARTESIAN_POINT ( 'NONE',  ( 38.31606138205700063, -22.22127907754186893, 75.30501292736998664 ) ) ;
#14559=CARTESIAN_POINT ( 'NONE',  ( 43.31606138205700063, -5.204193249396277032, 83.30501292736992980 ) ) ;
#14595=CARTESIAN_POINT ( 'NONE',  ( 33.31606138205700773, -11.22674583108233115, 81.40610939240433197 ) ) ;
#14607=CARTESIAN_POINT ( 'NONE',  ( 37.66883992158368955, -22.12333347212302925, 75.80539787555638043 ) ) ;
#14646=ORIENTED_EDGE ( 'NONE', *, *, #2147, .F. ) ;
#14659=ORIENTED_EDGE ( 'NONE', *, *, #20604, .T. ) ;
#14660=CARTESIAN_POINT ( 'NONE',  ( 40.31606138205700773, -20.32127907754186680, 75.99695190479390305 ) ) ;
#14679=AXIS2_PLACEMENT_3D ( 'NONE', #19896, #18345, #22200 ) ;
#14699=ORIENTED_EDGE ( 'NONE', *, *, #17781, .F. ) ;
#14712=LINE ( 'NONE', #3375, #10082 ) ;
#14716=AXIS2_PLACEMENT_3D ( 'NONE', #12297, #20266, #11917 ) ;
#14725=LINE ( 'NONE', #22712, #25013 ) ;
#14729=CARTESIAN_POINT ( 'NONE',  ( 36.31606138205700063, -20.32127907754186680, 75.99695190479390305 ) ) ;
#14743=SURFACE_STYLE_USAGE ( .BOTH. , #12957 ) ;
#14751=VERTEX_POINT ( 'NONE', #18518 ) ;
#14752=EDGE_CURVE ( 'NONE', #17171, #6977, #2964, .T. ) ;
#14765=CARTESIAN_POINT ( 'NONE',  ( 40.31606138205700773, -20.22127907754186893, 75.50705395623725735 ) ) ;
#14769=VERTEX_POINT ( 'NONE', #16841 ) ;
#14786=CARTESIAN_POINT ( 'NONE',  ( 40.31606138205700773, -7.204193249396275256, 83.11277699141410835 ) ) ;
#14790=CARTESIAN_POINT ( 'NONE',  ( 39.91050633825327054, -5.951964217243578048, 82.77254663560049153 ) ) ;
#14821=CARTESIAN_POINT ( 'NONE',  ( 39.54692359221319009, -21.81983708080221973, 75.31129620181626194 ) ) ;
#14840=CARTESIAN_POINT ( 'NONE',  ( 36.57656417722905928, -21.26713369642283524, 75.85247656039494757 ) ) ;
#14849=DIRECTION ( 'NONE',  ( 0.000000000000000000, -1.000000000000000000, 2.999999999999999839E-15 ) ) ;
#14854=CARTESIAN_POINT ( 'NONE',  ( 36.57656417722905928, -21.26713369642283880, 75.85247656039494757 ) ) ;
#14862=EDGE_LOOP ( 'NONE', ( #15463, #19302, #563, #471 ) ) ;
#14863=VERTEX_POINT ( 'NONE', #18772 ) ;
#14883=DIRECTION ( 'NONE',  ( 1.000000000000000000, 0.000000000000000000, 0.000000000000000000 ) ) ;
#14884=CARTESIAN_POINT ( 'NONE',  ( 37.68611352887096189, -5.296788164819011158, 82.80469560528126749 ) ) ;
#14912=CARTESIAN_POINT ( 'NONE',  ( 38.31606138205700063, -5.204193249396280585, 82.80001292736993435 ) ) ;
#14923=AXIS2_PLACEMENT_3D ( 'NONE', #22387, #14529, #12615 ) ;
#14940=ORIENTED_EDGE ( 'NONE', *, *, #1676, .F. ) ;
#14944=PLANE ( 'NONE',  #11406 ) ;
#14953=VERTEX_POINT ( 'NONE', #17607 ) ;
#14972=CARTESIAN_POINT ( 'NONE',  ( 37.66883992158368955, -22.11812637443705043, 75.30036834061758100 ) ) ;
#14986=PRODUCT_DEFINITION_FORMATION_WITH_SPECIFIED_SOURCE ( 'ANY', '', #2305, .NOT_KNOWN. ) ;
#14990=CARTESIAN_POINT ( 'NONE',  ( 37.09113907096683960, -21.82847486639043311, 75.81287845682257398 ) ) ;
#15041=CARTESIAN_POINT ( 'NONE',  ( 33.31606138205700773, -5.204193249396277032, 83.30501292736992980 ) ) ;
#15045=ORIENTED_EDGE ( 'NONE', *, *, #7893, .F. ) ;
#15046=CARTESIAN_POINT ( 'NONE',  ( 33.31606138205700773, -4.357181138186123626, 83.30501292736992980 ) ) ;
#15094=CARTESIAN_POINT ( 'NONE',  ( 37.09113907096683960, -21.80759215409126739, 75.30824661320679070 ) ) ;
#15096=CARTESIAN_POINT ( 'NONE',  ( 33.31606138205700773, -26.06829118875199924, 75.30501292736998664 ) ) ;
#15106=VECTOR ( 'NONE', #20651, 1000.000000000000000 ) ;
#15111=CARTESIAN_POINT ( 'NONE',  ( 36.31606138205700063, -6.942307388142325841, 83.16359031225202614 ) ) ;
#15125=DIRECTION ( 'NONE',  ( 0.000000000000000000, 1.000000000000000000, -2.921639538487253867E-15 ) ) ;
#15132=ORIENTED_EDGE ( 'NONE', *, *, #3125, .F. ) ;
#15156=EDGE_CURVE ( 'NONE', #24251, #15261, #2381, .T. ) ;
#15171=AXIS2_PLACEMENT_3D ( 'NONE', #24894, #7273, #15125 ) ;
#15185=VERTEX_POINT ( 'NONE', #20169 ) ;
#15193=CARTESIAN_POINT ( 'NONE',  ( 36.80507328770344344, -5.887228176602778973, 83.28319385500074645 ) ) ;
#15219=CARTESIAN_POINT ( 'NONE',  ( 37.66883992158368955, -22.12333347212302925, 75.80539787555638043 ) ) ;
#15224=CARTESIAN_POINT ( 'NONE',  ( 33.31606138205700773, -16.48551471403133206, 77.11349248448009064 ) ) ;
#15237=CARTESIAN_POINT ( 'NONE',  ( 36.36697178183959522, -6.614802349578126517, 82.70773085854241913 ) ) ;
#15261=VERTEX_POINT ( 'NONE', #24768 ) ;
#15295=CARTESIAN_POINT ( 'NONE',  ( 39.64148445914975127, -5.677091398499680253, 82.79421705341921722 ) ) ;
#15305=EDGE_LOOP ( 'NONE', ( #906, #22090, #5993, #22915, #22543 ) ) ;
#15324=CIRCLE ( 'NONE', #14103, 10.00000000000000000 ) ;
#15361=VECTOR ( 'NONE', #5225, 1000.000000000000000 ) ;
#15363=CARTESIAN_POINT ( 'NONE',  ( 36.99159426505191561, -5.699776791028273948, 83.29373111488995107 ) ) ;
#15409=VERTEX_POINT ( 'NONE', #11659 ) ;
#15427=CARTESIAN_POINT ( 'NONE',  ( 39.82611197195675601, -5.853806544725726368, 82.78428315609090760 ) ) ;
#15429=AXIS2_PLACEMENT_3D ( 'NONE', #20862, #24706, #6824 ) ;
#15463=ORIENTED_EDGE ( 'NONE', *, *, #15480, .F. ) ;
#15480=EDGE_CURVE ( 'NONE', #11231, #6167, #3645, .T. ) ;
#15487=CARTESIAN_POINT ( 'NONE',  ( 37.31005363372398165, -5.470823058559972196, 83.30693154845657489 ) ) ;
#15524=AXIS2_PLACEMENT_3D ( 'NONE', #21024, #23065, #9563 ) ;
#15546=AXIS2_PLACEMENT_3D ( 'NONE', #6324, #19978, #2189 ) ;
#15549=CARTESIAN_POINT ( 'NONE',  ( 39.91050633825327054, -5.990123355027524354, 83.28119501657926094 ) ) ;
#15561=EDGE_CURVE ( 'NONE', #4563, #24251, #18634, .T. ) ;
#15562=AXIS2_PLACEMENT_3D ( 'NONE', #16826, #20562, #8978 ) ;
#15580=CARTESIAN_POINT ( 'NONE',  ( 39.64097644196145609, -21.75034832497118842, 75.82127938882237572 ) ) ;
#15590=CARTESIAN_POINT ( 'NONE',  ( 36.31606138205700063, -7.108955154158179468, 82.62193108360246185 ) ) ;
#15614=DIRECTION ( 'NONE',  ( 1.000000000000000000, 0.000000000000000000, 0.000000000000000000 ) ) ;
#15622=VERTEX_POINT ( 'NONE', #21940 ) ;
#15691=EDGE_CURVE ( 'NONE', #6977, #11231, #4306, .T. ) ;
#15714=CARTESIAN_POINT ( 'NONE',  ( 38.31606138205700063, -22.22127907754186893, 75.81001292736998209 ) ) ;
#15730=ORIENTED_EDGE ( 'NONE', *, *, #15930, .T. ) ;
#15765=ADVANCED_FACE ( 'NONE', ( #18209 ), #18457, .F. ) ;
#15770=ORIENTED_EDGE ( 'NONE', *, *, #13038, .T. ) ;
#15771=ORIENTED_EDGE ( 'NONE', *, *, #19001, .T. ) ;
#15775=DIRECTION ( 'NONE',  ( 0.000000000000000000, -1.000000000000000000, 2.775557561562891351E-15 ) ) ;
#15780=CARTESIAN_POINT ( 'NONE',  ( 36.31606138205700063, -16.48551471403133206, 77.11349248448009064 ) ) ;
#15810=PLANE ( 'NONE',  #4093 ) ;
#15844=ORIENTED_EDGE ( 'NONE', *, *, #6421, .T. ) ;
#15875=ORIENTED_EDGE ( 'NONE', *, *, #8487, .T. ) ;
#15880=ORIENTED_EDGE ( 'NONE', *, *, #20761, .T. ) ;
#15917=VECTOR ( 'NONE', #18186, 1000.000000000000000 ) ;
#15919=CARTESIAN_POINT ( 'NONE',  ( 38.05466885408097255, -22.20915446671475735, 75.80998910758448517 ) ) ;
#15923=ORIENTED_EDGE ( 'NONE', *, *, #21150, .F. ) ;
#15930=EDGE_CURVE ( 'NONE', #11231, #24067, #24815, .T. ) ;
#15939=ORIENTED_EDGE ( 'NONE', *, *, #3446, .F. ) ;
#15958=CARTESIAN_POINT ( 'NONE',  ( 38.83707137437546919, -22.15992917496056691, 75.81017972364469415 ) ) ;
#15966=FACE_OUTER_BOUND ( 'NONE', #2843, .T. ) ;
#15983=DIRECTION ( 'NONE',  ( 1.000000000000000000, 0.000000000000000000, 0.000000000000000000 ) ) ;
#15993=CARTESIAN_POINT ( 'NONE',  ( 33.31606138205700773, -16.77230293220685198, 77.52306850662458260 ) ) ;
#16014=EDGE_LOOP ( 'NONE', ( #15939, #3613, #617, #3515, #7479, #1347, #22505 ) ) ;
#16015=DIRECTION ( 'NONE',  ( 0.000000000000000000, -1.000000000000000000, 4.625929269271485322E-15 ) ) ;
#16048=CARTESIAN_POINT ( 'NONE',  ( 37.66883992158368955, -22.12338502244167060, 75.81039767295206389 ) ) ;
#16059=DIRECTION ( 'NONE',  ( 0.000000000000000000, -3.225463739888140187E-15, -1.000000000000000000 ) ) ;
#16069=CIRCLE ( 'NONE', #24694, 9.500000000000000000 ) ;
#16089=CARTESIAN_POINT ( 'NONE',  ( 39.32240756636089429, -21.96791893307624832, 75.80813956697402034 ) ) ;
#16092=ORIENTED_EDGE ( 'NONE', *, *, #3804, .T. ) ;
#16097=DIRECTION ( 'NONE',  ( 0.000000000000000000, 1.000000000000000000, -2.921639538487253867E-15 ) ) ;
#16143=( NAMED_UNIT ( * ) PLANE_ANGLE_UNIT ( ) SI_UNIT ( $, .RADIAN. ) );
#16171=CARTESIAN_POINT ( 'NONE',  ( 36.41626118072728246, -20.92866386383740718, 75.89769837076177339 ) ) ;
#16176=EDGE_LOOP ( 'NONE', ( #4476, #23569, #13005, #14084 ) ) ;
#16178=EDGE_CURVE ( 'NONE', #23726, #3683, #10440, .T. ) ;
#16195=CARTESIAN_POINT ( 'NONE',  ( 43.31606138205700063, -4.357181138186127178, 82.80501292736992980 ) ) ;
#16214=DIRECTION ( 'NONE',  ( 1.000000000000000000, 0.000000000000000000, 0.000000000000000000 ) ) ;
#16227=DIRECTION ( 'NONE',  ( 0.000000000000000000, 2.999999999999999839E-15, 1.000000000000000000 ) ) ;
#16270=DIRECTION ( 'NONE',  ( 1.000000000000000000, 0.000000000000000000, 0.000000000000000000 ) ) ;
#16316=ORIENTED_EDGE ( 'NONE', *, *, #15561, .F. ) ;
#16333=CARTESIAN_POINT ( 'NONE',  ( 39.82744760895728575, -21.53778768028494994, 75.32795621999423474 ) ) ;
#16381=VECTOR ( 'NONE', #20434, 1000.000000000000000 ) ;
#16385=CARTESIAN_POINT ( 'NONE',  ( 38.31606138205700063, -22.22127907754186893, 75.30501292736998664 ) ) ;
#16395=FACE_OUTER_BOUND ( 'NONE', #14862, .T. ) ;
#16399=CARTESIAN_POINT ( 'NONE',  ( 33.31606138205700773, -22.22127907754187959, 75.30501292736998664 ) ) ;
#16401=CARTESIAN_POINT ( 'NONE',  ( 38.05217264712879199, -5.216721506228226168, 82.80003502201218168 ) ) ;
#16406=VERTEX_POINT ( 'NONE', #9157 ) ;
#16418=SURFACE_STYLE_FILL_AREA ( #12457 ) ;
#16457=LINE ( 'NONE', #3056, #2754 ) ;
#16459=CARTESIAN_POINT ( 'NONE',  ( 40.05520938202761982, -6.159673327590979852, 82.75478415414899303 ) ) ;
#16461=ORIENTED_EDGE ( 'NONE', *, *, #1239, .T. ) ;
#16467=VECTOR ( 'NONE', #10152, 1000.000000000000000 ) ;
#16474=CARTESIAN_POINT ( 'NONE',  ( 40.04430115328838724, -6.141487559858251899, 82.76153007216328206 ) ) ;
#16529=CARTESIAN_POINT ( 'NONE',  ( 37.09309150775561648, -5.596477263455031270, 82.79255245176237565 ) ) ;
#16557=CARTESIAN_POINT ( 'NONE',  ( 36.31606138205700063, -16.77230293220685198, 77.52306850662458260 ) ) ;
#16625=ORIENTED_EDGE ( 'NONE', *, *, #18303, .T. ) ;
#16643=ORIENTED_EDGE ( 'NONE', *, *, #21723, .T. ) ;
#16649=CARTESIAN_POINT ( 'NONE',  ( 36.51558096900348005, -21.15836054580815784, 75.86898487248532774 ) ) ;
#16652=LINE ( 'NONE', #11118, #10905 ) ;
#16698=LINE ( 'NONE', #20437, #12345 ) ;
#16720=CARTESIAN_POINT ( 'NONE',  ( 38.83610899671118943, -5.265395967213828854, 82.79985564382789676 ) ) ;
#16748=CARTESIAN_POINT ( 'NONE',  ( 40.11656585159207822, -21.15771639874553500, 75.86402839307550039 ) ) ;
#16764=PLANE ( 'NONE',  #9907 ) ;
#16771=DIRECTION ( 'NONE',  ( -0.000000000000000000, 0.5735764363510447161, -0.8191520442889929088 ) ) ;
#16791=CARTESIAN_POINT ( 'NONE',  ( 38.18531088334250967, -5.204193249396280585, 82.80501292736992980 ) ) ;
#16826=CARTESIAN_POINT ( 'NONE',  ( 33.31606138205700773, -5.204193249396356968, 72.80501292736992980 ) ) ;
#16841=CARTESIAN_POINT ( 'NONE',  ( 38.31606138205700063, -5.204193249396280585, 82.80501292736992980 ) ) ;
#16844=AXIS2_PLACEMENT_3D ( 'NONE', #12025, #3760, #17558 ) ;
#16879=DIRECTION ( 'NONE',  ( 0.000000000000000000, 2.999999999999999839E-15, 1.000000000000000000 ) ) ;
#16886=CARTESIAN_POINT ( 'NONE',  ( 38.31606138205700063, -5.204193249396277032, 83.30501292736992980 ) ) ;
#16911=CARTESIAN_POINT ( 'NONE',  ( 36.57656417722905928, -21.21640831487187739, 75.34994987701170999 ) ) ;
#16935=EDGE_LOOP ( 'NONE', ( #24049, #9846, #9867, #17952 ) ) ;
#16939=CARTESIAN_POINT ( 'NONE',  ( 43.31606138205700063, -16.48551471403133206, 77.11349248448009064 ) ) ;
#16943=VERTEX_POINT ( 'NONE', #37 ) ;
#16954=DIRECTION ( 'NONE',  ( 1.000000000000000000, 0.000000000000000000, 0.000000000000000000 ) ) ;
#16987=DIRECTION ( 'NONE',  ( 0.000000000000000000, 0.8191520442889929088, 0.5735764363510444941 ) ) ;
#17038=DIRECTION ( 'NONE',  ( 1.000000000000000000, 0.000000000000000000, 0.000000000000000000 ) ) ;
#17041=CARTESIAN_POINT ( 'NONE',  ( 36.32862050049384806, -20.47969909242301156, 75.45699727914595201 ) ) ;
#17052=EDGE_CURVE ( 'NONE', #19510, #16406, #5721, .T. ) ;
#17056=EDGE_CURVE ( 'NONE', #3232, #8101, #588, .T. ) ;
#17061=CARTESIAN_POINT ( 'NONE',  ( 36.36697178183959522, -6.685332804587225120, 83.20286675510105567 ) ) ;
#17116=CARTESIAN_POINT ( 'NONE',  ( 40.11623881305710881, -6.323019409765026744, 83.24594533976426192 ) ) ;
#17121=ORIENTED_EDGE ( 'NONE', *, *, #8809, .T. ) ;
#17141=EDGE_CURVE ( 'NONE', #8838, #16943, #6481, .T. ) ;
#17160=CARTESIAN_POINT ( 'NONE',  ( 40.31606138205700773, -26.06829118875199214, 77.52306850662461102 ) ) ;
#17165=CARTESIAN_POINT ( 'NONE',  ( 38.05466885408097255, -22.20850315994778867, 75.29993782803930458 ) ) ;
#17171=VERTEX_POINT ( 'NONE', #24361 ) ;
#17199=AXIS2_PLACEMENT_3D ( 'NONE', #3026, #8591, #2764 ) ;
#17237=CARTESIAN_POINT ( 'NONE',  ( 33.31606138205700773, -10.93995761290683255, 80.99653337025984001 ) ) ;
#17253=DIRECTION ( 'NONE',  ( 0.000000000000000000, -3.225463739888140187E-15, -1.000000000000000000 ) ) ;
#17272=EDGE_LOOP ( 'NONE', ( #4949, #17692, #7816, #6007, #8677, #11814, #1106 ) ) ;
#17292=CARTESIAN_POINT ( 'NONE',  ( 33.31606138205700773, -16.77230293220685198, 77.52306850662458260 ) ) ;
#17300=EDGE_CURVE ( 'NONE', #21524, #21641, #19595, .T. ) ;
#17338=CARTESIAN_POINT ( 'NONE',  ( 40.31606138205700773, -4.357181138186154712, 72.80501292736992980 ) ) ;
#17362=CARTESIAN_POINT ( 'NONE',  ( 38.96303889229209716, -5.307214332739725648, 83.30462760643098363 ) ) ;
#17367=CARTESIAN_POINT ( 'NONE',  ( 36.31606138205700063, -26.06829118875199924, 75.30501292736998664 ) ) ;
#17393=CARTESIAN_POINT ( 'NONE',  ( 37.09309150775561648, -5.616297516291425929, 83.29717550927296088 ) ) ;
#17403=VECTOR ( 'NONE', #12553, 1000.000000000000000 ) ;
#17417=DIRECTION ( 'NONE',  ( 0.000000000000000000, -3.289120579329467819E-15, -1.000000000000000000 ) ) ;
#17437=CARTESIAN_POINT ( 'NONE',  ( 38.31606138205700063, -5.204193249396277032, 83.31006292736994112 ) ) ;
#17458=B_SPLINE_CURVE_WITH_KNOTS ( 'NONE', 3,
 ( #2953, #10715, #10838, #1286, #18561, #4652, #1024, #8908, #18435, #766, #4772, #24717, #16748, #24583, #20755, #22675 ),
 .UNSPECIFIED., .F., .F.,
 ( 4, 2, 2, 2, 2, 2, 2, 4 ),
 ( 0.000000000000000000, 0.1250000000000006106, 0.2499999999999996947, 0.3750000000000002776, 0.5000000000000008882, 0.6249999999999982236, 0.7499999999999987788, 1.000000000000000000 ),
 .UNSPECIFIED. ) ;
#17482=( GEOMETRIC_REPRESENTATION_CONTEXT ( 3 ) GLOBAL_UNCERTAINTY_ASSIGNED_CONTEXT ( ( #5148 ) ) GLOBAL_UNIT_ASSIGNED_CONTEXT ( ( #8304, #19765, #8053 ) ) REPRESENTATION_CONTEXT ( 'NONE', 'WORKASPACE' ) );
#17501=CARTESIAN_POINT ( 'NONE',  ( 38.57734783014581836, -5.216343248895277895, 82.80503566129729620 ) ) ;
#17526=CARTESIAN_POINT ( 'NONE',  ( 33.31606138205700773, -1.357181138186128067, 82.80501292736991559 ) ) ;
#17541=LINE ( 'NONE', #15590, #23458 ) ;
#17543=DIRECTION ( 'NONE',  ( 1.000000000000000000, 0.000000000000000000, 0.000000000000000000 ) ) ;
#17558=DIRECTION ( 'NONE',  ( 0.000000000000000000, -2.999999999999999839E-15, -1.000000000000000000 ) ) ;
#17561=CARTESIAN_POINT ( 'NONE',  ( 36.99159426505191561, -5.700015143112625360, 83.29877568887539496 ) ) ;
#17602=VECTOR ( 'NONE', #10682, 1000.000000000000000 ) ;
#17607=CARTESIAN_POINT ( 'NONE',  ( 43.31606138205700063, -26.06829118875199569, 75.80501292736998664 ) ) ;
#17612=EDGE_CURVE ( 'NONE', #2946, #15409, #3788, .T. ) ;
#17646=VECTOR ( 'NONE', #24171, 1000.000000000000000 ) ;
#17655=VERTEX_POINT ( 'NONE', #14559 ) ;
#17656=CARTESIAN_POINT ( 'NONE',  ( 38.44690133353662276, -22.22127907754186893, 75.81001292736998209 ) ) ;
#17670=ORIENTED_EDGE ( 'NONE', *, *, #20567, .T. ) ;
#17692=ORIENTED_EDGE ( 'NONE', *, *, #1676, .T. ) ;
#17706=VECTOR ( 'NONE', #2735, 1000.000000000000000 ) ;
#17711=DIRECTION ( 'NONE',  ( 1.000000000000000000, 0.000000000000000000, 0.000000000000000000 ) ) ;
#17741=LINE ( 'NONE', #20392, #11720 ) ;
#17753=PLANE ( 'NONE',  #9455 ) ;
#17758=VERTEX_POINT ( 'NONE', #16195 ) ;
#17770=DIRECTION ( 'NONE',  ( -1.000000000000000000, 0.000000000000000000, 0.000000000000000000 ) ) ;
#17781=EDGE_CURVE ( 'NONE', #1739, #18120, #22377, .T. ) ;
#17787=CARTESIAN_POINT ( 'NONE',  ( 38.58006293444520196, -22.20876388569947935, 75.80498974974848636 ) ) ;
#17794=VECTOR ( 'NONE', #19406, 1000.000000000000000 ) ;
#17796=CARTESIAN_POINT ( 'NONE',  ( 33.31606138205700773, -22.22127907754180853, 85.30501292736998664 ) ) ;
#17802=CARTESIAN_POINT ( 'NONE',  ( 33.31606138205700773, -5.204193249396356968, 72.80501292736992980 ) ) ;
#17819=AXIS2_PLACEMENT_3D ( 'NONE', #8043, #6732, #17038 ) ;
#17842=ORIENTED_EDGE ( 'NONE', *, *, #13010, .T. ) ;
#17847=EDGE_CURVE ( 'NONE', #11458, #14769, #12983, .T. ) ;
#17894=VERTEX_POINT ( 'NONE', #21087 ) ;
#17918=DIRECTION ( 'NONE',  ( 0.000000000000000000, 2.999999999999999839E-15, 1.000000000000000000 ) ) ;
#17925=DIRECTION ( 'NONE',  ( 1.000000000000000000, 0.000000000000000000, 0.000000000000000000 ) ) ;
#17944=PLANE ( 'NONE',  #7142 ) ;
#17947=LINE ( 'NONE', #19868, #24224 ) ;
#17950=DIRECTION ( 'NONE',  ( 0.000000000000000000, -1.000000000000000000, 4.382459307730880209E-15 ) ) ;
#17952=ORIENTED_EDGE ( 'NONE', *, *, #15156, .T. ) ;
#17969=FACE_OUTER_BOUND ( 'NONE', #8774, .T. ) ;
#17999=CARTESIAN_POINT ( 'NONE',  ( 36.32862050049384806, -20.56764888167150929, 75.95432206938126285 ) ) ;
#18016=CARTESIAN_POINT ( 'NONE',  ( 40.31606138205700773, -29.06829118875199924, 75.30501292737000085 ) ) ;
#18031=AXIS2_PLACEMENT_3D ( 'NONE', #9521, #19045, #9768 ) ;
#18120=VERTEX_POINT ( 'NONE', #6004 ) ;
#18127=ORIENTED_EDGE ( 'NONE', *, *, #7202, .T. ) ;
#18152=CARTESIAN_POINT ( 'NONE',  ( 43.31606138205700063, -5.204193249396356968, 72.80501292736992980 ) ) ;
#18154=LINE ( 'NONE', #11988, #17646 ) ;
#18179=CARTESIAN_POINT ( 'NONE',  ( 38.31606138205700063, -5.204193249396280585, 82.80501292736992980 ) ) ;
#18186=DIRECTION ( 'NONE',  ( 0.000000000000000000, 0.8191520442889929088, 0.5735764363510444941 ) ) ;
#18193=AXIS2_PLACEMENT_3D ( 'NONE', #17292, #16771, #6853 ) ;
#18209=FACE_OUTER_BOUND ( 'NONE', #1423, .T. ) ;
#18222=EDGE_CURVE ( 'NONE', #6167, #12702, #23334, .T. ) ;
#18223=CARTESIAN_POINT ( 'NONE',  ( 33.31606138205700773, -5.204193249396356968, 72.80501292736992980 ) ) ;
#18259=DIRECTION ( 'NONE',  ( 1.000000000000000000, 0.000000000000000000, 0.000000000000000000 ) ) ;
#18288=CARTESIAN_POINT ( 'NONE',  ( 33.31606138205700773, -5.204193249396280585, 82.80501292736992980 ) ) ;
#18295=CARTESIAN_POINT ( 'NONE',  ( 40.11656585159207822, -21.10117404812173802, 75.36211584159703136 ) ) ;
#18303=EDGE_CURVE ( 'NONE', #8101, #4612, #16457, .T. ) ;
#18343=ORIENTED_EDGE ( 'NONE', *, *, #16178, .F. ) ;
#18345=DIRECTION ( 'NONE',  ( -0.000000000000000000, 0.5735764363510447161, -0.8191520442889929088 ) ) ;
#18346=EDGE_CURVE ( 'NONE', #24769, #3808, #10932, .T. ) ;
#18378=LINE ( 'NONE', #8594, #16381 ) ;
#18406=DIRECTION ( 'NONE',  ( 0.000000000000000000, -0.1999999999999926281, 0.9797958971132726402 ) ) ;
#18415=CARTESIAN_POINT ( 'NONE',  ( 39.20536636138601949, -22.01751967489730077, 75.30696121124701392 ) ) ;
#18435=CARTESIAN_POINT ( 'NONE',  ( 39.64097644196145609, -21.75010033615993876, 75.81628532166148204 ) ) ;
#18457=PLANE ( 'NONE',  #17819 ) ;
#18469=EDGE_CURVE ( 'NONE', #19510, #5267, #21345, .T. ) ;
#18472=EDGE_CURVE ( 'NONE', #24795, #536, #9385, .T. ) ;
#18508=CARTESIAN_POINT ( 'NONE',  ( 37.80737592653075296, -5.262488812442727593, 82.80487014872778673 ) ) ;
#18513=DIRECTION ( 'NONE',  ( 1.000000000000000000, 0.000000000000000000, 0.000000000000000000 ) ) ;
#18518=CARTESIAN_POINT ( 'NONE',  ( 36.31606138205700063, -29.06829118875199924, 75.30501292737000085 ) ) ;
#18524=VECTOR ( 'NONE', #8696, 1000.000000000000000 ) ;
#18530=CARTESIAN_POINT ( 'NONE',  ( 40.25357836725066818, -6.620057786443027226, 82.69997634557660149 ) ) ;
#18537=CARTESIAN_POINT ( 'NONE',  ( 39.90994555940143584, -21.43601452184545764, 75.33022986137839894 ) ) ;
#18561=CARTESIAN_POINT ( 'NONE',  ( 38.96215273200666473, -22.12375471166958008, 75.80539210339577494 ) ) ;
#18569=CARTESIAN_POINT ( 'NONE',  ( 33.31606138205700773, -4.357181138186127178, 82.80501292736992980 ) ) ;
#18573=ORIENTED_EDGE ( 'NONE', *, *, #20567, .F. ) ;
#18581=CARTESIAN_POINT ( 'NONE',  ( 37.79585267494195477, -22.16019180447545622, 75.81017787406068464 ) ) ;
#18596=CARTESIAN_POINT ( 'NONE',  ( 36.31606138205700063, -6.858712374802629519, 82.66539206659815875 ) ) ;
#18634=CIRCLE ( 'NONE', #5471, 3.000000000000002665 ) ;
#18687=VECTOR ( 'NONE', #16954, 1000.000000000000000 ) ;
#18689=VECTOR ( 'NONE', #14466, 1000.000000000000000 ) ;
#18716=CARTESIAN_POINT ( 'NONE',  ( 38.31606138205700063, -22.22127907754186893, 75.80501292736997243 ) ) ;
#18731=CARTESIAN_POINT ( 'NONE',  ( 38.31606138205700063, -5.204193249396280585, 82.80501292736992980 ) ) ;
#18757=FACE_OUTER_BOUND ( 'NONE', #11976, .T. ) ;
#18761=CARTESIAN_POINT ( 'NONE',  ( 36.31606138205700063, -7.108955154158179468, 82.62193108360246185 ) ) ;
#18763=EDGE_CURVE ( 'NONE', #7399, #5590, #24655, .T. ) ;
#18772=CARTESIAN_POINT ( 'NONE',  ( 40.31606138205700773, -16.77230293220685198, 77.52306850662458260 ) ) ;
#18783=CARTESIAN_POINT ( 'NONE',  ( 40.05520938202761982, -6.160151306619628286, 82.75976152844953049 ) ) ;
#18791=ORIENTED_EDGE ( 'NONE', *, *, #17847, .F. ) ;
#18804=ORIENTED_EDGE ( 'NONE', *, *, #23166, .T. ) ;
#18833=ADVANCED_FACE ( 'NONE', ( #706 ), #22236, .T. ) ;
#18835=CARTESIAN_POINT ( 'NONE',  ( 36.41626118072728246, -20.85991497674728024, 75.39736199887265400 ) ) ;
#18916=AXIS2_PLACEMENT_3D ( 'NONE', #17367, #9771, #21616 ) ;
#18934=ORIENTED_EDGE ( 'NONE', *, *, #11957, .T. ) ;
#18947=LINE ( 'NONE', #13022, #1583 ) ;
#18952=CARTESIAN_POINT ( 'NONE',  ( 40.31606138205700773, -20.22127907754186893, 75.50705395623725735 ) ) ;
#18954=ORIENTED_EDGE ( 'NONE', *, *, #9749, .T. ) ;
#18966=LINE ( 'NONE', #1305, #10898 ) ;
#18970=CARTESIAN_POINT ( 'NONE',  ( 36.51558096900348005, -21.10126295790812989, 75.36210271246490322 ) ) ;
#18974=CARTESIAN_POINT ( 'NONE',  ( 33.31606138205700773, -29.06829118875199924, 75.30501292737000085 ) ) ;
#18986=CARTESIAN_POINT ( 'NONE',  ( 37.42710149357921523, -5.407787168292675695, 83.30316041875967414 ) ) ;
#19001=EDGE_CURVE ( 'NONE', #21641, #23726, #4874, .T. ) ;
#19045=DIRECTION ( 'NONE',  ( 1.000000000000000000, 0.000000000000000000, 0.000000000000000000 ) ) ;
#19078=CARTESIAN_POINT ( 'NONE',  ( 39.33009355364794146, -21.96558760913888264, 75.30775939357174309 ) ) ;
#19082=ORIENTED_EDGE ( 'NONE', *, *, #18472, .T. ) ;
#19100=CARTESIAN_POINT ( 'NONE',  ( 37.31068429205632953, -21.95526386996113999, 75.30827953495455063 ) ) ;
#19116=CARTESIAN_POINT ( 'NONE',  ( 38.05217264712879199, -5.217360829629674512, 83.31008614951315394 ) ) ;
#19140=LINE ( 'NONE', #7547, #5469 ) ;
#19165=CARTESIAN_POINT ( 'NONE',  ( 39.32110845963273960, -5.470022085696077063, 83.30190618885059450 ) ) ;
#19171=ADVANCED_FACE ( 'NONE', ( #25457 ), #1391, .F. ) ;
#19206=DIRECTION ( 'NONE',  ( -0.000000000000000000, 0.1904761904761826663, -0.9816918156232541381 ) ) ;
#19215=CARTESIAN_POINT ( 'NONE',  ( 36.72121174906109786, -21.43519715395374803, 75.33535480072937673 ) ) ;
#19220=PRODUCT_DEFINITION ( 'UNKNOWN', '', #14986, #14181 ) ;
#19223=SHAPE_DEFINITION_REPRESENTATION ( #19584, #11141 ) ;
#19234=CARTESIAN_POINT ( 'NONE',  ( 36.31606138205700063, -20.32127907754186680, 75.99695190479390305 ) ) ;
#19284=CARTESIAN_POINT ( 'NONE',  ( 38.57734783014581836, -5.216950748870224253, 83.30503679799366523 ) ) ;
#19288=CARTESIAN_POINT ( 'NONE',  ( 39.91050633825327054, -5.989745541782124150, 83.27615889399532989 ) ) ;
#19302=ORIENTED_EDGE ( 'NONE', *, *, #15691, .F. ) ;
#19306=VERTEX_POINT ( 'NONE', #19550 ) ;
#19313=EDGE_CURVE ( 'NONE', #11231, #5640, #9391, .T. ) ;
#19315=VECTOR ( 'NONE', #17918, 1000.000000000000000 ) ;
#19317=CARTESIAN_POINT ( 'NONE',  ( 37.67019652925851148, -5.306778407178573964, 83.30463327861060918 ) ) ;
#19322=CARTESIAN_POINT ( 'NONE',  ( 40.06556677248106269, -21.22556384466594182, 75.35168022282572053 ) ) ;
#19358=CARTESIAN_POINT ( 'NONE',  ( 37.09309150775561648, -5.596673503582127118, 82.79754871965852203 ) ) ;
#19386=PLANE ( 'NONE',  #8640 ) ;
#19406=DIRECTION ( 'NONE',  ( 0.000000000000000000, 6.469446951953614816E-15, 1.000000000000000000 ) ) ;
#19412=CARTESIAN_POINT ( 'NONE',  ( 39.64148445914975127, -5.700736305954877459, 83.29367725972169012 ) ) ;
#19440=CARTESIAN_POINT ( 'NONE',  ( 36.57819145821473228, -6.205787318996375035, 83.25770116091617012 ) ) ;
#19460=FACE_OUTER_BOUND ( 'NONE', #742, .T. ) ;
#19508=ADVANCED_FACE ( 'NONE', ( #18757 ), #22492, .T. ) ;
#19510=VERTEX_POINT ( 'NONE', #24660 ) ;
#19511=CARTESIAN_POINT ( 'NONE',  ( 43.31606138205700063, -29.06829118875199924, 75.30501292737000085 ) ) ;
#19514=VECTOR ( 'NONE', #787, 1000.000000000000000 ) ;
#19535=ORIENTED_EDGE ( 'NONE', *, *, #891, .F. ) ;
#19550=CARTESIAN_POINT ( 'NONE',  ( 33.31606138205700773, -5.204193249396280585, 82.80501292736992980 ) ) ;
#19584=PRODUCT_DEFINITION_SHAPE ( 'NONE', 'NONE',  #19220 ) ;
#19595=LINE ( 'NONE', #21405, #1693 ) ;
#19634=EDGE_CURVE ( 'NONE', #2156, #14477, #18378, .T. ) ;
#19662=CARTESIAN_POINT ( 'NONE',  ( 36.32862050049384806, -20.56677809167894111, 75.94939806155714734 ) ) ;
#19703=CARTESIAN_POINT ( 'NONE',  ( 38.31606138205700063, -22.22127907754186893, 75.80501292736997243 ) ) ;
#19722=CARTESIAN_POINT ( 'NONE',  ( 40.31606138205700773, -4.357181138186127178, 82.80501292736992980 ) ) ;
#19752=CARTESIAN_POINT ( 'NONE',  ( 40.31606138205700773, -10.93995761290683255, 80.99653337025984001 ) ) ;
#19765=( NAMED_UNIT ( * ) PLANE_ANGLE_UNIT ( ) SI_UNIT ( $, .RADIAN. ) );
#19774=LINE ( 'NONE', #1630, #13568 ) ;
#19792=AXIS2_PLACEMENT_3D ( 'NONE', #5749, #21844, #65 ) ;
#19810=CARTESIAN_POINT ( 'NONE',  ( 36.72059563575756158, -21.43489111338284658, 75.33538682622121030 ) ) ;
#19831=VECTOR ( 'NONE', #18513, 1000.000000000000000 ) ;
#19833=CARTESIAN_POINT ( 'NONE',  ( 33.31606138205700773, -5.204193249396280585, 82.80501292736992980 ) ) ;
#19858=VECTOR ( 'NONE', #2666, 1000.000000000000000 ) ;
#19868=CARTESIAN_POINT ( 'NONE',  ( 33.31606138205700773, -16.48551471403133206, 77.11349248448009064 ) ) ;
#19896=CARTESIAN_POINT ( 'NONE',  ( 33.31606138205700773, -16.48551471403133206, 77.11349248448009064 ) ) ;
#19910=ORIENTED_EDGE ( 'NONE', *, *, #17141, .F. ) ;
#19919=ADVANCED_FACE ( 'NONE', ( #2361 ), #11928, .T. ) ;
#19934=DIRECTION ( 'NONE',  ( 1.000000000000000000, 0.000000000000000000, 0.000000000000000000 ) ) ;
#19968=CARTESIAN_POINT ( 'NONE',  ( 38.83707137437546919, -22.15989686853476925, 75.80517981147842477 ) ) ;
#19978=DIRECTION ( 'NONE',  ( 1.000000000000000000, 0.000000000000000000, 0.000000000000000000 ) ) ;
#19979=ORIENTED_EDGE ( 'NONE', *, *, #19313, .T. ) ;
#19993=DIRECTION ( 'NONE',  ( 1.000000000000000000, 0.000000000000000000, 0.000000000000000000 ) ) ;
#20003=ORIENTED_EDGE ( 'NONE', *, *, #5341, .T. ) ;
#20006=CARTESIAN_POINT ( 'NONE',  ( 40.31606138205700773, -16.48551471403133206, 77.11349248448009064 ) ) ;
#20018=PLANE ( 'NONE',  #14679 ) ;
#20020=SURFACE_SIDE_STYLE ('',( #5991 ) ) ;
#20028=CARTESIAN_POINT ( 'NONE',  ( 38.31606138205700063, -22.22127907754186893, 75.80501292736997243 ) ) ;
#20046=CIRCLE ( 'NONE', #13461, 9.500000000000001776 ) ;
#20056=CARTESIAN_POINT ( 'NONE',  ( 40.31606138205700773, -7.204193249396275256, 83.11277699141410835 ) ) ;
#20064=CARTESIAN_POINT ( 'NONE',  ( 36.80477597196090045, -21.53774254971854418, 75.32796878085879655 ) ) ;
#20070=CARTESIAN_POINT ( 'NONE',  ( 40.31606138205700773, -22.22127907754180853, 85.30501292736998664 ) ) ;
#20079=DIRECTION ( 'NONE',  ( -1.000000000000000000, 0.000000000000000000, 0.000000000000000000 ) ) ;
#20099=EDGE_LOOP ( 'NONE', ( #4908, #7577, #8335, #3437, #8701, #11028, #6160 ) ) ;
#20100=CARTESIAN_POINT ( 'NONE',  ( 38.82716350840370723, -5.250869752214502917, 82.80533778410890022 ) ) ;
#20120=AXIS2_PLACEMENT_3D ( 'NONE', #1294, #24857, #7102 ) ;
#20144=ORIENTED_EDGE ( 'NONE', *, *, #24193, .F. ) ;
#20158=EDGE_CURVE ( 'NONE', #6977, #14863, #14725, .T. ) ;
#20169=CARTESIAN_POINT ( 'NONE',  ( 36.31606138205700063, -7.204193249396275256, 83.11277699141410835 ) ) ;
#20203=CYLINDRICAL_SURFACE ( 'NONE', #5054, 10.00000000000000000 ) ;
#20216=CARTESIAN_POINT ( 'NONE',  ( 40.11656585159207822, -21.10173941565100009, 75.36713447021789136 ) ) ;
#20266=DIRECTION ( 'NONE',  ( 0.000000000000000000, 2.999999999999999839E-15, 1.000000000000000000 ) ) ;
#20268=ADVANCED_BREP_SHAPE_REPRESENTATION ( '', ( #25265, #2000 ), #17482 ) ;
#20286=CARTESIAN_POINT ( 'NONE',  ( 38.18494427818247061, -22.22127907754186893, 75.80501292736997243 ) ) ;
#20297=ORIENTED_EDGE ( 'NONE', *, *, #18346, .F. ) ;
#20310=EDGE_LOOP ( 'NONE', ( #11562, #5011, #23496, #21743 ) ) ;
#20323=CARTESIAN_POINT ( 'NONE',  ( 36.36526940127878760, -20.73543518430840749, 75.41293983993888617 ) ) ;
#20335=FACE_OUTER_BOUND ( 'NONE', #21517, .T. ) ;
#20392=CARTESIAN_POINT ( 'NONE',  ( 36.31606138205700063, -10.93995761290683255, 80.99653337025984001 ) ) ;
#20394=ORIENTED_EDGE ( 'NONE', *, *, #17056, .T. ) ;
#20402=LINE ( 'NONE', #12441, #17706 ) ;
#20408=ORIENTED_EDGE ( 'NONE', *, *, #2374, .T. ) ;
#20410=CARTESIAN_POINT ( 'NONE',  ( 33.31606138205700773, -5.204193249396356968, 72.80501292736992980 ) ) ;
#20426=ADVANCED_FACE ( 'NONE', ( #6213 ), #7899, .T. ) ;
#20434=DIRECTION ( 'NONE',  ( 0.000000000000000000, 2.999999999999999839E-15, 1.000000000000000000 ) ) ;
#20435=EDGE_CURVE ( 'NONE', #723, #15261, #7769, .T. ) ;
#20437=CARTESIAN_POINT ( 'NONE',  ( 33.31606138205700773, -5.204193249396277032, 83.30501292736992980 ) ) ;
#20438=CARTESIAN_POINT ( 'NONE',  ( 36.31606138205701484, -6.852252720116931428, 82.67173867183331026 ) ) ;
#20478=DIRECTION ( 'NONE',  ( 0.000000000000000000, 1.000000000000000000, -2.775557561562891351E-15 ) ) ;
#20501=ADVANCED_FACE ( 'NONE', ( #5963 ), #14205, .T. ) ;
#20516=AXIS2_PLACEMENT_3D ( 'NONE', #23497, #2108, #12184 ) ;
#20531=CARTESIAN_POINT ( 'NONE',  ( 36.57819145821473228, -6.157615413744179200, 82.75497663158847672 ) ) ;
#20549=VECTOR ( 'NONE', #13978, 1000.000000000000000 ) ;
#20562=DIRECTION ( 'NONE',  ( 1.000000000000000000, 0.000000000000000000, 0.000000000000000000 ) ) ;
#20567=EDGE_CURVE ( 'NONE', #6977, #5267, #17947, .T. ) ;
#20580=CARTESIAN_POINT ( 'NONE',  ( 36.31606138205700063, -11.22674583108233115, 81.40610939240433197 ) ) ;
#20584=DIRECTION ( 'NONE',  ( 1.000000000000000000, 0.000000000000000000, 0.000000000000000000 ) ) ;
#20589=CARTESIAN_POINT ( 'NONE',  ( 39.54057891361352972, -5.597492753917878261, 82.79251829992152523 ) ) ;
#20594=EDGE_CURVE ( 'NONE', #19306, #21783, #22295, .T. ) ;
#20604=EDGE_CURVE ( 'NONE', #17894, #15622, #4658, .T. ) ;
#20610=ORIENTED_EDGE ( 'NONE', *, *, #8626, .F. ) ;
#20621=DIRECTION ( 'NONE',  ( 0.000000000000000000, -2.999999999999999839E-15, -1.000000000000000000 ) ) ;
#20626=CARTESIAN_POINT ( 'NONE',  ( 33.31606138205700773, -10.93995761290683255, 80.99653337025984001 ) ) ;
#20642=CARTESIAN_POINT ( 'NONE',  ( 36.31606138205700063, -20.35033391287788973, 75.47555661361914758 ) ) ;
#20651=DIRECTION ( 'NONE',  ( -0.000000000000000000, 0.5735764363510441610, -0.8191520442889931308 ) ) ;
#20653=CIRCLE ( 'NONE', #23446, 3.000000000000000000 ) ;
#20663=CARTESIAN_POINT ( 'NONE',  ( 36.36697178183959522, -6.614097045028025867, 82.70277949957684882 ) ) ;
#20676=ORIENTED_EDGE ( 'NONE', *, *, #2611, .F. ) ;
#20696=VECTOR ( 'NONE', #23366, 1000.000000000000000 ) ;
#20698=CARTESIAN_POINT ( 'NONE',  ( 37.11263866765397523, -5.585986591960282688, 82.79779740004656219 ) ) ;
#20718=CARTESIAN_POINT ( 'NONE',  ( 39.64148445914975127, -5.700736305954877459, 83.29367725972169012 ) ) ;
#20723=CARTESIAN_POINT ( 'NONE',  ( 40.30346352106939634, -6.862507256641427134, 82.66731276300377829 ) ) ;
#20724=AXIS2_PLACEMENT_3D ( 'NONE', #23864, #23490, #4936 ) ;
#20729=DIRECTION ( 'NONE',  ( -0.000000000000000000, 1.000000000000000000, -3.225463739888140187E-15 ) ) ;
#20732=EDGE_LOOP ( 'NONE', ( #14659, #18804, #4357, #21961 ) ) ;
#20755=CARTESIAN_POINT ( 'NONE',  ( 40.31606138205700773, -20.56964486282017646, 75.94625445116911067 ) ) ;
#20761=EDGE_CURVE ( 'NONE', #15185, #7399, #6146, .T. ) ;
#20778=DIRECTION ( 'NONE',  ( -1.000000000000000000, 0.000000000000000000, 0.000000000000000000 ) ) ;
#20780=CARTESIAN_POINT ( 'NONE',  ( 36.41626118072728246, -20.92798318178700612, 75.89274454529751779 ) ) ;
#20794=DIRECTION ( 'NONE',  ( 0.000000000000000000, -0.5735764363510444941, 0.8191520442889929088 ) ) ;
#20809=EDGE_LOOP ( 'NONE', ( #24938, #15132, #19082, #8798, #6953 ) ) ;
#20825=LINE ( 'NONE', #14765, #4865 ) ;
#20832=EDGE_CURVE ( 'NONE', #1739, #17171, #4954, .T. ) ;
#20859=CARTESIAN_POINT ( 'NONE',  ( 40.31606138205700773, -16.77230293220685198, 77.52306850662458260 ) ) ;
#20862=CARTESIAN_POINT ( 'NONE',  ( 33.31606138205700773, -1.357181138186128067, 82.80501292736991559 ) ) ;
#20882=CLOSED_SHELL ( 'NONE', ( #976, #283, #211, #8654, #22071, #7837, #21016, #2313, #12603, #12353, #21535, #3595, #4980, #22681, #9355, #23084, #15765, #18833, #1725, #7099, #6861, #3713, #19919, #20426, #5005, #11163, #5021, #20501, #10744, #2145, #19508, #13654, #7840, #3257, #2464, #25364, #5318, #7249, #22026, #2392, #5632, #19171 ) ) ;
#20901=CARTESIAN_POINT ( 'NONE',  ( 37.79585267494195477, -22.16015963634850650, 75.80517796092046012 ) ) ;
#20918=CARTESIAN_POINT ( 'NONE',  ( 36.57819145821473228, -6.205787318996375035, 83.25770116091617012 ) ) ;
#20929=ORIENTED_EDGE ( 'NONE', *, *, #11683, .T. ) ;
#20959=DIRECTION ( 'NONE',  ( 0.000000000000000000, -9.938893903907220328E-15, -1.000000000000000000 ) ) ;
#20974=CARTESIAN_POINT ( 'NONE',  ( 39.82611197195675601, -5.886287209492222949, 83.28324666752695293 ) ) ;
#20975=DIRECTION ( 'NONE',  ( -0.000000000000000000, 0.5735764363510463815, -0.8191520442889914655 ) ) ;
#20976=EDGE_CURVE ( 'NONE', #19306, #3683, #7999, .T. ) ;
#20980=CARTESIAN_POINT ( 'NONE',  ( 40.25357836725066818, -6.692310083303524060, 83.20492142726308771 ) ) ;
#21010=CARTESIAN_POINT ( 'NONE',  ( 38.31606138205700063, -22.22127907754186893, 75.30501292736998664 ) ) ;
#21016=ADVANCED_FACE ( 'NONE', ( #11867 ), #1886, .F. ) ;
#21024=CARTESIAN_POINT ( 'NONE',  ( 36.31606138205700063, -4.357181138186127178, 82.80501292736992980 ) ) ;
#21031=CARTESIAN_POINT ( 'NONE',  ( 36.41626118072728246, -20.85922748787637815, 75.39235863515375513 ) ) ;
#21046=CARTESIAN_POINT ( 'NONE',  ( 36.99159426505191561, -5.676177574760129296, 82.79426834405568059 ) ) ;
#21087=CARTESIAN_POINT ( 'NONE',  ( 33.31606138205700773, -10.93995761290683255, 80.99653337025984001 ) ) ;
#21091=VERTEX_POINT ( 'NONE', #15046 ) ;
#21105=CARTESIAN_POINT ( 'NONE',  ( 38.44711690269065940, -5.204193249396277032, 83.31006292736994112 ) ) ;
#21131=CARTESIAN_POINT ( 'NONE',  ( 36.31606138205700063, -16.48551471403133206, 77.11349248448009064 ) ) ;
#21133=CARTESIAN_POINT ( 'NONE',  ( 36.31606138205700063, -6.942307388142325841, 83.16359031225202614 ) ) ;
#21150=EDGE_CURVE ( 'NONE', #17655, #2946, #7325, .T. ) ;
#21157=CARTESIAN_POINT ( 'NONE',  ( 36.72121174906109786, -21.43480018258233954, 75.33032012337542938 ) ) ;
#21174=CARTESIAN_POINT ( 'NONE',  ( 36.57819145821473228, -6.206269038048873199, 83.26272840620944748 ) ) ;
#21178=ORIENTED_EDGE ( 'NONE', *, *, #20761, .F. ) ;
#21219=EDGE_CURVE ( 'NONE', #17655, #22871, #3456, .T. ) ;
#21229=CARTESIAN_POINT ( 'NONE',  ( 39.82611197195675601, -5.886615264206325193, 83.28828619899245211 ) ) ;
#21252=DIRECTION ( 'NONE',  ( 1.000000000000000000, 0.000000000000000000, 0.000000000000000000 ) ) ;
#21291=CARTESIAN_POINT ( 'NONE',  ( 38.18531088334250967, -5.204193249396277032, 83.31006292736994112 ) ) ;
#21299=ORIENTED_EDGE ( 'NONE', *, *, #18472, .F. ) ;
#21301=CARTESIAN_POINT ( 'NONE',  ( 40.31606138205700773, -11.22674583108233115, 81.40610939240433197 ) ) ;
#21302=EDGE_CURVE ( 'NONE', #5640, #16406, #19774, .T. ) ;
#21345=LINE ( 'NONE', #23019, #697 ) ;
#21349=CARTESIAN_POINT ( 'NONE',  ( 40.05520938202761982, -6.207949209480774222, 83.25749895850351834 ) ) ;
#21400=ORIENTED_EDGE ( 'NONE', *, *, #8626, .T. ) ;
#21405=CARTESIAN_POINT ( 'NONE',  ( 33.31606138205700773, -16.48551471403133206, 77.11349248448009064 ) ) ;
#21437=DIRECTION ( 'NONE',  ( 0.000000000000000000, 0.8191520442889929088, 0.5735764363510444941 ) ) ;
#21440=LINE ( 'NONE', #11667, #6507 ) ;
#21480=CARTESIAN_POINT ( 'NONE',  ( 38.83610899671118943, -5.268519173439224268, 83.30989761756769951 ) ) ;
#21482=EDGE_CURVE ( 'NONE', #4612, #24795, #25184, .T. ) ;
#21517=EDGE_LOOP ( 'NONE', ( #5212, #9103, #17670, #3546, #14699 ) ) ;
#21524=VERTEX_POINT ( 'NONE', #7137 ) ;
#21535=ADVANCED_FACE ( 'NONE', ( #2620 ), #9522, .T. ) ;
#21572=ORIENTED_EDGE ( 'NONE', *, *, #812, .F. ) ;
#21604=CARTESIAN_POINT ( 'NONE',  ( 36.31606138205700063, -20.44477830400171570, 75.97174273075597739 ) ) ;
#21609=CARTESIAN_POINT ( 'NONE',  ( 38.96303889229209716, -5.307214332739725648, 83.30462760643098363 ) ) ;
#21616=DIRECTION ( 'NONE',  ( 1.000000000000000000, 0.000000000000000000, 0.000000000000000000 ) ) ;
#21626=ORIENTED_EDGE ( 'NONE', *, *, #5219, .F. ) ;
#21641=VERTEX_POINT ( 'NONE', #15993 ) ;
#21646=B_SPLINE_SURFACE_WITH_KNOTS ( 'NONE', 1, 3, ( 
 ( #450, #7955, #17999, #321, #16171, #16649, #13748, #8201, #2129, #24024, #10011, #2848, #200, #16048, #18581, #15919, #919, #11824 ),
 ( #8811, #21604, #19662, #2003, #20780, #11372, #14840, #9067, #24990, #8928, #7375, #12799, #13305, #15219, #20901, #3236, #11250, #18716 ),
 ( #13048, #23072, #17041, #11116, #18835, #3372, #13178, #19215, #5313, #3114, #22697, #19100, #24869, #1438, #5437, #9321, #24740, #5056 ),
 ( #7246, #20642, #1174, #10984, #21031, #18970, #16911, #21157, #7117, #1551, #15094, #22951, #9442, #14972, #22829, #17165, #5190, #3498 ) ),
 .UNSPECIFIED., .F., .F., .F.,
 ( 2, 1, 1, 2 ),
 ( 4, 2, 2, 2, 2, 2, 2, 2, 4 ),
 ( -0.01000000000000000021, 0.000000000000000000, 1.000000000000000000, 1.010099999999999998 ),
 ( 0.000000000000000000, 0.0003925198642609844754, 0.0007850397285219689507, 0.001177559592782951962, 0.001570079457043939853, 0.001962599321304919937, 0.002355119185565904792, 0.002747639049826890081, 0.003140158914087874936 ),
 .UNSPECIFIED. ) ;
#21655=EDGE_CURVE ( 'NONE', #536, #19510, #20046, .T. ) ;
#21664=CARTESIAN_POINT ( 'NONE',  ( 36.31606138205700063, -16.48551471403133206, 77.11349248448009064 ) ) ;
#21709=CARTESIAN_POINT ( 'NONE',  ( 33.31606138205700773, -22.22127907754186893, 75.80501292736997243 ) ) ;
#21723=EDGE_CURVE ( 'NONE', #22871, #17758, #14209, .T. ) ;
#21743=ORIENTED_EDGE ( 'NONE', *, *, #18469, .T. ) ;
#21760=AXIS2_PLACEMENT_3D ( 'NONE', #6553, #487, #22017 ) ;
#21783=VERTEX_POINT ( 'NONE', #18569 ) ;
#21810=VERTEX_POINT ( 'NONE', #2963 ) ;
#21817=DIRECTION ( 'NONE',  ( 0.000000000000000000, -2.999999999999999839E-15, -1.000000000000000000 ) ) ;
#21844=DIRECTION ( 'NONE',  ( 1.000000000000000000, 0.000000000000000000, 0.000000000000000000 ) ) ;
#21896=CARTESIAN_POINT ( 'NONE',  ( 40.26527270485448184, -20.81444828448985973, 75.91197220037939530 ) ) ;
#21940=CARTESIAN_POINT ( 'NONE',  ( 36.31606138205700063, -10.93995761290683255, 80.99653337025984001 ) ) ;
#21942=CIRCLE ( 'NONE', #1357, 10.00000000000000000 ) ;
#21957=AXIS2_PLACEMENT_3D ( 'NONE', #11031, #22137, #6433 ) ;
#21961=ORIENTED_EDGE ( 'NONE', *, *, #2147, .T. ) ;
#21967=DIRECTION ( 'NONE',  ( 1.000000000000000000, 0.000000000000000000, 0.000000000000000000 ) ) ;
#22017=DIRECTION ( 'NONE',  ( 0.000000000000000000, -1.000000000000000000, 2.999999999999999839E-15 ) ) ;
#22020=CARTESIAN_POINT ( 'NONE',  ( 40.05426416818898616, -21.21860219669770231, 75.34973409106177655 ) ) ;
#22026=ADVANCED_FACE ( 'NONE', ( #9309 ), #11100, .T. ) ;
#22071=ADVANCED_FACE ( 'NONE', ( #2423 ), #4626, .F. ) ;
#22073=( NAMED_UNIT ( * ) SI_UNIT ( $, .STERADIAN. ) SOLID_ANGLE_UNIT ( ) );
#22090=ORIENTED_EDGE ( 'NONE', *, *, #25431, .T. ) ;
#22118=CARTESIAN_POINT ( 'NONE',  ( 37.25504499466181585, -21.91763188072224011, 75.30955569975962760 ) ) ;
#22137=DIRECTION ( 'NONE',  ( 1.000000000000000000, 0.000000000000000000, 0.000000000000000000 ) ) ;
#22156=VECTOR ( 'NONE', #5347, 1000.000000000000000 ) ;
#22157=EDGE_CURVE ( 'NONE', #15261, #14953, #7389, .T. ) ;
#22164=EDGE_CURVE ( 'NONE', #19306, #14769, #11995, .T. ) ;
#22200=DIRECTION ( 'NONE',  ( 0.000000000000000000, 0.8191520442889929088, 0.5735764363510447161 ) ) ;
#22226=( NAMED_UNIT ( * ) PLANE_ANGLE_UNIT ( ) SI_UNIT ( $, .RADIAN. ) );
#22236=PLANE ( 'NONE',  #17199 ) ;
#22264=DIRECTION ( 'NONE',  ( 0.000000000000000000, -1.000000000000000000, 2.999999999999999839E-15 ) ) ;
#22272=ORIENTED_EDGE ( 'NONE', *, *, #13214, .T. ) ;
#22273=ORIENTED_EDGE ( 'NONE', *, *, #15156, .F. ) ;
#22295=LINE ( 'NONE', #8664, #13953 ) ;
#22333=DIRECTION ( 'NONE',  ( -1.000000000000000000, 0.000000000000000000, 0.000000000000000000 ) ) ;
#22338=CARTESIAN_POINT ( 'NONE',  ( 38.05466885408097255, -22.20914808198024559, 75.80498909504116511 ) ) ;
#22372=CARTESIAN_POINT ( 'NONE',  ( 36.52583090115293629, -6.250151542416438666, 82.75087430736850536 ) ) ;
#22377=LINE ( 'NONE', #6656, #19831 ) ;
#22387=CARTESIAN_POINT ( 'NONE',  ( 33.31606138205700773, -22.22127907754180853, 85.30501292736998664 ) ) ;
#22390=CARTESIAN_POINT ( 'NONE',  ( 36.31606138205700063, -26.06829118875199569, 75.80501292736998664 ) ) ;
#22401=CARTESIAN_POINT ( 'NONE',  ( 38.58006293444520196, -22.20810519139199002, 75.30498852987368252 ) ) ;
#22402=CARTESIAN_POINT ( 'NONE',  ( 33.31606138205700773, -11.22674583108233115, 81.40610939240433197 ) ) ;
#22419=DIRECTION ( 'NONE',  ( -1.000000000000000000, 0.000000000000000000, 0.000000000000000000 ) ) ;
#22461=CARTESIAN_POINT ( 'NONE',  ( 36.99159426505191561, -5.675941582597428869, 82.78927371634733845 ) ) ;
#22492=CYLINDRICAL_SURFACE ( 'NONE', #15562, 10.50000000000000000 ) ;
#22494=DIRECTION ( 'NONE',  ( 0.000000000000000000, -0.1999999999999969580, 0.9797958971132719741 ) ) ;
#22495=EDGE_CURVE ( 'NONE', #14751, #8838, #22606, .T. ) ;
#22505=ORIENTED_EDGE ( 'NONE', *, *, #15561, .T. ) ;
#22524=CARTESIAN_POINT ( 'NONE',  ( 39.53940869104339839, -21.80888753443083772, 75.31325401218029469 ) ) ;
#22537=DIRECTION ( 'NONE',  ( 1.000000000000000000, 0.000000000000000000, 0.000000000000000000 ) ) ;
#22543=ORIENTED_EDGE ( 'NONE', *, *, #22164, .T. ) ;
#22589=CARTESIAN_POINT ( 'NONE',  ( 36.72255525790973252, -5.950843403820127442, 82.77262573514066446 ) ) ;
#22606=CIRCLE ( 'NONE', #18916, 3.000000000000002665 ) ;
#22644=CARTESIAN_POINT ( 'NONE',  ( 40.11623881305710881, -6.323019409765026744, 83.24594533976426192 ) ) ;
#22649=CARTESIAN_POINT ( 'NONE',  ( 40.31606138205700773, -7.108955154158179468, 82.62193108360246185 ) ) ;
#22653=VECTOR ( 'NONE', #1273, 1000.000000000000000 ) ;
#22675=CARTESIAN_POINT ( 'NONE',  ( 40.31606138205700773, -20.32127907754186680, 75.99695190479390305 ) ) ;
#22681=ADVANCED_FACE ( 'NONE', ( #12215 ), #17753, .F. ) ;
#22697=CARTESIAN_POINT ( 'NONE',  ( 37.09113907096683960, -21.80780096054036221, 75.31329243205692592 ) ) ;
#22712=CARTESIAN_POINT ( 'NONE',  ( 40.31606138205700773, -16.48551471403133206, 77.11349248448009064 ) ) ;
#22739=CIRCLE ( 'NONE', #14923, 9.500000000000001776 ) ;
#22774=CARTESIAN_POINT ( 'NONE',  ( 40.25357836725066818, -6.620766072854777917, 82.70492630226405595 ) ) ;
#22813=ORIENTED_EDGE ( 'NONE', *, *, #7374, .F. ) ;
#22829=CARTESIAN_POINT ( 'NONE',  ( 37.79585267494195477, -22.15691033384591080, 75.30013673462515555 ) ) ;
#22844=CARTESIAN_POINT ( 'NONE',  ( 36.51585873400316018, -6.269825903680327883, 82.74874648979978531 ) ) ;
#22871=VERTEX_POINT ( 'NONE', #12720 ) ;
#22892=CARTESIAN_POINT ( 'NONE',  ( 39.91050633825327054, -5.989745541782124150, 83.27615889399532989 ) ) ;
#22915=ORIENTED_EDGE ( 'NONE', *, *, #12266, .T. ) ;
#22922=LINE ( 'NONE', #17526, #1991 ) ;
#22941=EDGE_CURVE ( 'NONE', #11458, #17655, #16698, .T. ) ;
#22951=CARTESIAN_POINT ( 'NONE',  ( 37.31068429205632953, -21.95512953228131892, 75.30323118459136822 ) ) ;
#22968=CARTESIAN_POINT ( 'NONE',  ( 36.31606138205700063, -7.204193249396275256, 83.11277699141410835 ) ) ;
#23003=ORIENTED_EDGE ( 'NONE', *, *, #7202, .F. ) ;
#23019=CARTESIAN_POINT ( 'NONE',  ( 43.31606138205700063, -16.77230293220685198, 77.52306850662458260 ) ) ;
#23022=CARTESIAN_POINT ( 'NONE',  ( 40.21566563214662438, -6.564967302039574903, 83.21717579561996558 ) ) ;
#23049=CARTESIAN_POINT ( 'NONE',  ( 36.51585873400316018, -6.323107536394523720, 83.24593316792127951 ) ) ;
#23065=DIRECTION ( 'NONE',  ( 0.000000000000000000, 2.999999999999999839E-15, 1.000000000000000000 ) ) ;
#23072=CARTESIAN_POINT ( 'NONE',  ( 36.31606138205700063, -20.35127826328909251, 75.48051798356576114 ) ) ;
#23084=ADVANCED_FACE ( 'NONE', ( #25297 ), #19386, .T. ) ;
#23091=CARTESIAN_POINT ( 'NONE',  ( 36.51585873400316018, -6.323107536394523720, 83.24593316792127951 ) ) ;
#23103=DIRECTION ( 'NONE',  ( 0.000000000000000000, -0.5735764363510444941, 0.8191520442889929088 ) ) ;
#23110=ORIENTED_EDGE ( 'NONE', *, *, #1239, .F. ) ;
#23136=LINE ( 'NONE', #11571, #17794 ) ;
#23146=CARTESIAN_POINT ( 'NONE',  ( 39.54057891361352972, -5.597689502044176812, 82.79751455073319732 ) ) ;
#23166=EDGE_CURVE ( 'NONE', #15622, #3232, #8310, .T. ) ;
#23202=VECTOR ( 'NONE', #21437, 1000.000000000000000 ) ;
#23276=CARTESIAN_POINT ( 'NONE',  ( 40.31606138205700773, -7.204193249396275256, 83.11277699141410835 ) ) ;
#23282=CARTESIAN_POINT ( 'NONE',  ( 40.31606138205700773, -7.108955154158179468, 82.62193108360246185 ) ) ;
#23334=CIRCLE ( 'NONE', #4829, 10.50000000000000000 ) ;
#23354=VECTOR ( 'NONE', #1312, 1000.000000000000000 ) ;
#23366=DIRECTION ( 'NONE',  ( 0.000000000000000000, -0.5735764363510444941, 0.8191520442889929088 ) ) ;
#23382=CYLINDRICAL_SURFACE ( 'NONE', #19792, 10.00000000000000000 ) ;
#23386=( GEOMETRIC_REPRESENTATION_CONTEXT ( 3 ) GLOBAL_UNCERTAINTY_ASSIGNED_CONTEXT ( ( #6129 ) ) GLOBAL_UNIT_ASSIGNED_CONTEXT ( ( #12706, #22226, #6769 ) ) REPRESENTATION_CONTEXT ( 'NONE', 'WORKASPACE' ) );
#23388=EDGE_CURVE ( 'NONE', #3808, #1739, #3481, .T. ) ;
#23397=CARTESIAN_POINT ( 'NONE',  ( 38.57734783014581836, -5.216956884619976087, 83.31008680947429923 ) ) ;
#23410=EDGE_CURVE ( 'NONE', #3683, #21091, #20402, .T. ) ;
#23431=DIRECTION ( 'NONE',  ( -0.000000000000000000, 0.5735764363510447161, -0.8191520442889929088 ) ) ;
#23438=CARTESIAN_POINT ( 'NONE',  ( 40.11656585159207822, -21.15827616857647797, 75.86899733230406184 ) ) ;
#23446=AXIS2_PLACEMENT_3D ( 'NONE', #19722, #17417, #7886 ) ;
#23458=VECTOR ( 'NONE', #19206, 999.9999999999998863 ) ;
#23466=DIRECTION ( 'NONE',  ( 0.000000000000000000, -2.999999999999999839E-15, -1.000000000000000000 ) ) ;
#23490=DIRECTION ( 'NONE',  ( -1.000000000000000000, 0.000000000000000000, 0.000000000000000000 ) ) ;
#23496=ORIENTED_EDGE ( 'NONE', *, *, #17052, .F. ) ;
#23497=CARTESIAN_POINT ( 'NONE',  ( 43.31606138205700063, -5.204193249396277032, 83.30501292736992980 ) ) ;
#23544=CARTESIAN_POINT ( 'NONE',  ( 33.31606138205700773, -5.204193249396280585, 82.80501292736992980 ) ) ;
#23564=CARTESIAN_POINT ( 'NONE',  ( 40.31606138205700773, -20.32227907754186802, 76.00185088427946312 ) ) ;
#23569=ORIENTED_EDGE ( 'NONE', *, *, #23166, .F. ) ;
#23640=EDGE_LOOP ( 'NONE', ( #13739, #17842, #24969, #7522 ) ) ;
#23680=DIRECTION ( 'NONE',  ( 0.000000000000000000, -1.000000000000000000, 2.775557561562891351E-15 ) ) ;
#23691=CARTESIAN_POINT ( 'NONE',  ( 39.20536636138601949, -22.02780952473084852, 75.81186282291122325 ) ) ;
#23700=CARTESIAN_POINT ( 'NONE',  ( 36.31606138205700063, -22.22127907754180853, 85.30501292736998664 ) ) ;
#23721=CARTESIAN_POINT ( 'NONE',  ( 43.31606138205700063, -22.22127907754180853, 85.30501292736998664 ) ) ;
#23726=VERTEX_POINT ( 'NONE', #22402 ) ;
#23814=CARTESIAN_POINT ( 'NONE',  ( 39.82744760895728575, -21.57230399584641845, 75.83179758371670687 ) ) ;
#23822=DIRECTION ( 'NONE',  ( 1.000000000000000000, 0.000000000000000000, 0.000000000000000000 ) ) ;
#23846=ORIENTED_EDGE ( 'NONE', *, *, #10592, .T. ) ;
#23864=CARTESIAN_POINT ( 'NONE',  ( 33.31606138205700773, -22.22127907754186893, 75.80501292736997243 ) ) ;
#23869=FILL_AREA_STYLE_COLOUR ( '', #24041 ) ;
#23939=CARTESIAN_POINT ( 'NONE',  ( 39.82744760895728575, -21.53744251712932822, 75.32291780635701173 ) ) ;
#23952=CARTESIAN_POINT ( 'NONE',  ( 39.76340311107733783, -5.792909836048790062, 82.78776523435020351 ) ) ;
#24024=CARTESIAN_POINT ( 'NONE',  ( 36.99021717747880444, -21.74946196664538078, 75.82133169473785017 ) ) ;
#24041=COLOUR_RGB ( '', 0.72549020, 0.75294118, 0.79215686) ;
#24042=CARTESIAN_POINT ( 'NONE',  ( 37.42666033486774069, -22.01378883779070961, 75.30711745748108399 ) ) ;
#24049=ORIENTED_EDGE ( 'NONE', *, *, #20435, .F. ) ;
#24067=VERTEX_POINT ( 'NONE', #23282 ) ;
#24085=DIRECTION ( 'NONE',  ( 0.000000000000000000, -1.000000000000000000, 2.999999999999999839E-15 ) ) ;
#24092=DIRECTION ( 'NONE',  ( 1.000000000000000000, 0.000000000000000000, 0.000000000000000000 ) ) ;
#24171=DIRECTION ( 'NONE',  ( 1.000000000000000000, 0.000000000000000000, 0.000000000000000000 ) ) ;
#24184=CARTESIAN_POINT ( 'NONE',  ( 38.58006293444520196, -22.20809853857948823, 75.29993851755294543 ) ) ;
#24193=EDGE_CURVE ( 'NONE', #21091, #21783, #9656, .T. ) ;
#24224=VECTOR ( 'NONE', #24092, 1000.000000000000000 ) ;
#24233=EDGE_CURVE ( 'NONE', #14953, #536, #25461, .T. ) ;
#24242=PRODUCT_CONTEXT ( 'NONE', #24918, 'mechanical' ) ;
#24245=EDGE_LOOP ( 'NONE', ( #13531, #11304, #20676, #8600 ) ) ;
#24250=CARTESIAN_POINT ( 'NONE',  ( 37.79523030992096011, -5.265654987800329145, 82.79985390080808827 ) ) ;
#24251=VERTEX_POINT ( 'NONE', #18016 ) ;
#24254=ORIENTED_EDGE ( 'NONE', *, *, #9912, .T. ) ;
#24255=EDGE_LOOP ( 'NONE', ( #12592, #4469, #3993, #10538 ) ) ;
#24302=CARTESIAN_POINT ( 'NONE',  ( 40.31606138205700773, -7.073990261058225926, 83.13804008194063044 ) ) ;
#24303=DIRECTION ( 'NONE',  ( 0.000000000000000000, 1.000000000000000000, -1.321694076934710205E-15 ) ) ;
#24305=CARTESIAN_POINT ( 'NONE',  ( 39.20459794252392527, -5.397853031073977625, 82.79825093644204514 ) ) ;
#24306=EDGE_CURVE ( 'NONE', #8101, #1739, #9560, .T. ) ;
#24310=CARTESIAN_POINT ( 'NONE',  ( 39.90994555940143584, -21.47565429014790794, 75.83375200144557482 ) ) ;
#24316=LINE ( 'NONE', #20859, #22653 ) ;
#24353=ORIENTED_EDGE ( 'NONE', *, *, #6264, .T. ) ;
#24361=CARTESIAN_POINT ( 'NONE',  ( 40.31606138205700773, -20.22127907754186893, 75.50705395623725735 ) ) ;
#24377=CARTESIAN_POINT ( 'NONE',  ( 36.72121174906109786, -21.47450125013314803, 75.83383770706140581 ) ) ;
#24442=CARTESIAN_POINT ( 'NONE',  ( 39.64097644196145609, -21.72505098633521214, 75.31183459773906463 ) ) ;
#24533=EDGE_LOOP ( 'NONE', ( #10889, #12034, #10914, #20929 ) ) ;
#24547=DIRECTION ( 'NONE',  ( 0.000000000000000000, -2.999999999999999839E-15, -1.000000000000000000 ) ) ;
#24550=AXIS2_PLACEMENT_3D ( 'NONE', #17160, #1546, #17543 ) ;
#24554=CARTESIAN_POINT ( 'NONE',  ( 38.57734783014581836, -5.216337173895527535, 82.80003564993033649 ) ) ;
#24558=CARTESIAN_POINT ( 'NONE',  ( 43.31606138205700063, -5.204193249396277032, 83.30501292736992980 ) ) ;
#24583=CARTESIAN_POINT ( 'NONE',  ( 40.26527270485448184, -20.81370745732132832, 75.90702589141309886 ) ) ;
#24655=LINE ( 'NONE', #16557, #5674 ) ;
#24660=CARTESIAN_POINT ( 'NONE',  ( 43.31606138205700063, -16.77230293220685198, 77.52306850662458260 ) ) ;
#24674=ORIENTED_EDGE ( 'NONE', *, *, #20158, .F. ) ;
#24684=LINE ( 'NONE', #2916, #11515 ) ;
#24686=LINE ( 'NONE', #10681, #3416 ) ;
#24689=CARTESIAN_POINT ( 'NONE',  ( 39.32110845963273960, -5.457236984521631307, 82.79705560817937737 ) ) ;
#24694=AXIS2_PLACEMENT_3D ( 'NONE', #23700, #6196, #16097 ) ;
#24706=DIRECTION ( 'NONE',  ( 0.000000000000000000, 1.000000000000000000, -2.999999999999999839E-15 ) ) ;
#24714=ORIENTED_EDGE ( 'NONE', *, *, #18222, .T. ) ;
#24717=CARTESIAN_POINT ( 'NONE',  ( 40.05426416818898616, -21.26921683217381798, 75.85227166721355729 ) ) ;
#24737=DIRECTION ( 'NONE',  ( 0.000000000000000000, -1.000000000000000000, 2.775557561562891351E-15 ) ) ;
#24740=CARTESIAN_POINT ( 'NONE',  ( 38.18494427818247061, -22.22127907754186893, 75.30501292736998664 ) ) ;
#24756=VECTOR ( 'NONE', #20959, 1000.000000000000000 ) ;
#24758=CARTESIAN_POINT ( 'NONE',  ( 36.80559154321147020, -21.57283688862124649, 75.82675744184658129 ) ) ;
#24768=CARTESIAN_POINT ( 'NONE',  ( 40.31606138205700773, -29.06829118875199924, 75.80501292737000085 ) ) ;
#24769=VERTEX_POINT ( 'NONE', #21709 ) ;
#24795=VERTEX_POINT ( 'NONE', #20028 ) ;
#24815=CIRCLE ( 'NONE', #4264, 10.00000000000000000 ) ;
#24857=DIRECTION ( 'NONE',  ( -0.000000000000000000, 0.5735764363510447161, -0.8191520442889929088 ) ) ;
#24869=CARTESIAN_POINT ( 'NONE',  ( 37.42719827050449055, -22.01767691212489808, 75.30695952225683243 ) ) ;
#24881=CARTESIAN_POINT ( 'NONE',  ( 36.80507328770344344, -5.887228176602778973, 83.28319385500074645 ) ) ;
#24894=CARTESIAN_POINT ( 'NONE',  ( 33.31606138205700773, -22.22127907754180853, 85.30501292736998664 ) ) ;
#24918=APPLICATION_CONTEXT ( 'automotive_design' ) ;
#24932=CARTESIAN_POINT ( 'NONE',  ( 39.20459794252392527, -5.407637742404325820, 83.30316191138764736 ) ) ;
#24938=ORIENTED_EDGE ( 'NONE', *, *, #13214, .F. ) ;
#24966=CARTESIAN_POINT ( 'NONE',  ( 38.18531088334250967, -5.204193249396277032, 83.30501292736992980 ) ) ;
#24969=ORIENTED_EDGE ( 'NONE', *, *, #18469, .F. ) ;
#24982=PLANE ( 'NONE',  #9084 ) ;
#24990=CARTESIAN_POINT ( 'NONE',  ( 36.80559154321147020, -21.57283688862124649, 75.82675744184658129 ) ) ;
#24993=FACE_OUTER_BOUND ( 'NONE', #6916, .T. ) ;
#25013=VECTOR ( 'NONE', #20794, 1000.000000000000000 ) ;
#25057=CARTESIAN_POINT ( 'NONE',  ( 38.44711690269065940, -5.204193249396277032, 83.30501292736992980 ) ) ;
#25063=DIRECTION ( 'NONE',  ( 1.000000000000000000, 0.000000000000000000, 0.000000000000000000 ) ) ;
#25088=CARTESIAN_POINT ( 'NONE',  ( 33.31606138205700773, -16.77230293220685198, 77.52306850662458260 ) ) ;
#25129=CARTESIAN_POINT ( 'NONE',  ( 37.67019652925851148, -5.301893399665129181, 82.80465135712294966 ) ) ;
#25164=ORIENTED_EDGE ( 'NONE', *, *, #24193, .T. ) ;
#25184=B_SPLINE_CURVE_WITH_KNOTS ( 'NONE', 3,
 ( #14729, #1064, #8827, #12816, #4698, #10879, #14854, #24377, #24758, #11001, #14990, #4812, #5077, #14607, #12943, #22338, #20286, #678 ),
 .UNSPECIFIED., .F., .F.,
 ( 4, 2, 2, 2, 2, 2, 2, 2, 4 ),
 ( 0.000000000000000000, 0.1250000000000000278, 0.2500000000000000555, 0.3749999999999996114, 0.5000000000000007772, 0.6249999999999994449, 0.7499999999999995559, 0.8749999999999998890, 1.000000000000000000 ),
 .UNSPECIFIED. ) ;
#25192=CARTESIAN_POINT ( 'NONE',  ( 40.25357836725066818, -6.691594714027675472, 83.19992197100876297 ) ) ;
#25226=CARTESIAN_POINT ( 'NONE',  ( 36.99159426505191561, -5.699776791028273948, 83.29373111488995107 ) ) ;
#25264=CARTESIAN_POINT ( 'NONE',  ( 37.79523030992096011, -5.268791411979726114, 83.30989578560070186 ) ) ;
#25265=MANIFOLD_SOLID_BREP ( 'NONE', #20882 ) ;
#25295=ORIENTED_EDGE ( 'NONE', *, *, #24233, .F. ) ;
#25297=FACE_OUTER_BOUND ( 'NONE', #12375, .T. ) ;
#25318=EDGE_CURVE ( 'NONE', #5267, #5640, #9347, .T. ) ;
#25321=CARTESIAN_POINT ( 'NONE',  ( 39.20459794252392527, -5.407637742404325820, 83.30316191138764736 ) ) ;
#25323=DIRECTION ( 'NONE',  ( 1.000000000000000000, 0.000000000000000000, 0.000000000000000000 ) ) ;
#25325=CARTESIAN_POINT ( 'NONE',  ( 38.44711690269065940, -5.204193249396277032, 83.30501292736992980 ) ) ;
#25364=ADVANCED_FACE ( 'NONE', ( #11660 ), #1340, .F. ) ;
#25412=PLANE ( 'NONE',  #12236 ) ;
#25418=DIRECTION ( 'NONE',  ( 0.000000000000000000, -1.000000000000000000, 2.999999999999999839E-15 ) ) ;
#25419=DIRECTION ( 'NONE',  ( 0.000000000000000000, -2.999999999999999839E-15, -1.000000000000000000 ) ) ;
#25431=EDGE_CURVE ( 'NONE', #4753, #15622, #6536, .T. ) ;
#25457=FACE_OUTER_BOUND ( 'NONE', #7207, .T. ) ;
#25461=LINE ( 'NONE', #9396, #16467 ) ;
#25484=DIRECTION ( 'NONE',  ( 0.000000000000000000, 0.8191520442889929088, 0.5735764363510447161 ) ) ;
ENDSEC;
END-ISO-10303-21;
